ISO-10303-21;
HEADER;
FILE_DESCRIPTION (('STEP AP214'),
    '1' );
FILE_NAME ('Plunger Actuator.step',
    '2026-10-09T19:32:29',
    ( '' ),
    ( '' ),
    'SwSTEP 2.0',
    'SolidWorks 2026',
    '' );
FILE_SCHEMA (( 'AUTOMOTIVE_DESIGN' ));
ENDSEC;

DATA;
#14=CARTESIAN_POINT ( 'NONE',  ( -7.186903215246500006E-16, 5.131370849898470254, 6.100000000000000533 ) ) ;
#21=CARTESIAN_POINT ( 'NONE',  ( -1.250000000000000000, 0.5999999999999999778, 7.599999999999999645 ) ) ;
#28=CARTESIAN_POINT ( 'NONE',  ( 0.5500000000000000444, 2.050000000000000266, 1.600000000000000089 ) ) ;
#42=ORIENTED_EDGE ( 'NONE', *, *, #5974, .F. ) ;
#51=PLANE ( 'NONE',  #9042 ) ;
#52=DIRECTION ( 'NONE',  ( -2.379049338482479710E-16, 0.000000000000000000, -1.000000000000000000 ) ) ;
#57=DIRECTION ( 'NONE',  ( 0.000000000000000000, 6.123233995736769734E-17, -1.000000000000000000 ) ) ;
#59=EDGE_LOOP ( 'NONE', ( #2998, #8111, #2641, #14217 ) ) ;
#77=LINE ( 'NONE', #14322, #1274 ) ;
#78=LINE ( 'NONE', #15272, #17717 ) ;
#88=AXIS2_PLACEMENT_3D ( 'NONE', #12369, #6813, #17991 ) ;
#91=LINE ( 'NONE', #17013, #9613 ) ;
#93=EDGE_CURVE ( 'NONE', #12376, #4659, #13727, .T. ) ;
#98=DIRECTION ( 'NONE',  ( -2.220446049250309876E-16, 1.000000000000000000, 0.000000000000000000 ) ) ;
#99=ORIENTED_EDGE ( 'NONE', *, *, #10473, .T. ) ;
#102=DIRECTION ( 'NONE',  ( 0.7071067811865480168, 0.7071067811865470176, 0.000000000000000000 ) ) ;
#104=CARTESIAN_POINT ( 'NONE',  ( -1.000000000000000000, -5.000000000000000000, 6.100000000000000533 ) ) ;
#105=ADVANCED_FACE ( 'NONE', ( #14933 ), #6784, .T. ) ;
#109=DIRECTION ( 'NONE',  ( -1.000000000000000000, 0.000000000000000000, 0.000000000000000000 ) ) ;
#111=EDGE_CURVE ( 'NONE', #2785, #786, #2714, .T. ) ;
#115=CARTESIAN_POINT ( 'NONE',  ( -1.000000000000000000, -5.000000000000000000, 6.100000000000000533 ) ) ;
#125=ORIENTED_EDGE ( 'NONE', *, *, #6265, .F. ) ;
#129=EDGE_CURVE ( 'NONE', #14329, #8376, #6958, .T. ) ;
#133=PLANE ( 'NONE',  #14387 ) ;
#138=VERTEX_POINT ( 'NONE', #2989 ) ;
#151=VECTOR ( 'NONE', #14058, 1000.000000000000000 ) ;
#152=DIRECTION ( 'NONE',  ( 5.887846720064179370E-16, 1.000000000000000000, 0.000000000000000000 ) ) ;
#171=CARTESIAN_POINT ( 'NONE',  ( 0.9000000000000000222, -10.00000000000000000, 6.100000000000000533 ) ) ;
#177=EDGE_CURVE ( 'NONE', #9615, #14727, #5673, .T. ) ;
#190=ORIENTED_EDGE ( 'NONE', *, *, #14281, .T. ) ;
#201=LINE ( 'NONE', #17127, #858 ) ;
#208=VECTOR ( 'NONE', #15083, 1000.000000000000000 ) ;
#210=ORIENTED_EDGE ( 'NONE', *, *, #3477, .T. ) ;
#217=PLANE ( 'NONE',  #15934 ) ;
#219=ORIENTED_EDGE ( 'NONE', *, *, #701, .F. ) ;
#231=CARTESIAN_POINT ( 'NONE',  ( 0.9000000000000000222, -10.00000000000000000, 3.799999999999999822 ) ) ;
#235=VECTOR ( 'NONE', #9014, 1000.000000000000000 ) ;
#236=ORIENTED_EDGE ( 'NONE', *, *, #9107, .F. ) ;
#238=PLANE ( 'NONE',  #6124 ) ;
#255=VECTOR ( 'NONE', #13621, 1000.000000000000000 ) ;
#256=AXIS2_PLACEMENT_3D ( 'NONE', #8428, #15667, #98 ) ;
#257=DIRECTION ( 'NONE',  ( -1.189524669241239855E-16, 1.000000000000000000, 0.000000000000000000 ) ) ;
#259=ADVANCED_FACE ( 'NONE', ( #15058 ), #2172, .T. ) ;
#272=ORIENTED_EDGE ( 'NONE', *, *, #15142, .T. ) ;
#275=DIRECTION ( 'NONE',  ( -1.000000000000000000, 0.000000000000000000, 0.000000000000000000 ) ) ;
#283=FACE_OUTER_BOUND ( 'NONE', #8177, .T. ) ;
#305=VERTEX_POINT ( 'NONE', #7812 ) ;
#315=ADVANCED_FACE ( 'NONE', ( #5219 ), #2456, .T. ) ;
#316=FACE_OUTER_BOUND ( 'NONE', #11871, .T. ) ;
#328=DIRECTION ( 'NONE',  ( 1.000000000000000000, 1.224646799147350002E-16, 0.000000000000000000 ) ) ;
#346=CARTESIAN_POINT ( 'NONE',  ( -1.250000000000000000, 0.5999999999999999778, 6.100000000000000533 ) ) ;
#356=VERTEX_POINT ( 'NONE', #17700 ) ;
#368=LINE ( 'NONE', #14, #4331 ) ;
#373=PLANE ( 'NONE',  #10593 ) ;
#374=EDGE_LOOP ( 'NONE', ( #16981, #5498, #13083, #14749 ) ) ;
#375=VECTOR ( 'NONE', #12826, 1000.000000000000000 ) ;
#416=CARTESIAN_POINT ( 'NONE',  ( -1.000000000000000000, -7.000000000000000000, 5.700000000000000178 ) ) ;
#426=ORIENTED_EDGE ( 'NONE', *, *, #18287, .T. ) ;
#436=EDGE_CURVE ( 'NONE', #3716, #6119, #18067, .T. ) ;
#438=CARTESIAN_POINT ( 'NONE',  ( 1.000000000000000000, -8.000000000000000000, 3.700000000000000178 ) ) ;
#440=DIRECTION ( 'NONE',  ( 2.018587317500279868E-16, -1.000000000000000000, -1.009293658750139934E-16 ) ) ;
#457=FACE_BOUND ( 'NONE', #15789, .T. ) ;
#458=VERTEX_POINT ( 'NONE', #936 ) ;
#471=ORIENTED_EDGE ( 'NONE', *, *, #11105, .F. ) ;
#477=DIRECTION ( 'NONE',  ( 0.000000000000000000, 0.000000000000000000, -1.000000000000000000 ) ) ;
#478=ORIENTED_EDGE ( 'NONE', *, *, #1154, .F. ) ;
#490=VERTEX_POINT ( 'NONE', #3889 ) ;
#491=LINE ( 'NONE', #17068, #7903 ) ;
#497=VECTOR ( 'NONE', #10509, 1000.000000000000000 ) ;
#531=VECTOR ( 'NONE', #12503, 1000.000000000000000 ) ;
#541=CARTESIAN_POINT ( 'NONE',  ( 1.399999999999999911, -5.500000000000000000, 5.100000000000000533 ) ) ;
#544=VECTOR ( 'NONE', #5083, 1000.000000000000000 ) ;
#550=DIRECTION ( 'NONE',  ( -1.000000000000000000, -8.881784197001249119E-17, -1.776356839400249824E-16 ) ) ;
#568=ORIENTED_EDGE ( 'NONE', *, *, #93, .F. ) ;
#575=ORIENTED_EDGE ( 'NONE', *, *, #10898, .F. ) ;
#582=EDGE_CURVE ( 'NONE', #14617, #14203, #6481, .T. ) ;
#584=FACE_BOUND ( 'NONE', #16591, .T. ) ;
#592=CARTESIAN_POINT ( 'NONE',  ( 1.828929293328490072E-16, 2.399999999999999911, 5.100000000000000533 ) ) ;
#598=ADVANCED_FACE ( 'NONE', ( #11204 ), #1488, .T. ) ;
#607=LINE ( 'NONE', #6245, #10557 ) ;
#619=LINE ( 'NONE', #17535, #497 ) ;
#620=VERTEX_POINT ( 'NONE', #1657 ) ;
#636=DIRECTION ( 'NONE',  ( 1.000000000000000000, 0.000000000000000000, 0.000000000000000000 ) ) ;
#638=ORIENTED_EDGE ( 'NONE', *, *, #18114, .F. ) ;
#656=ORIENTED_EDGE ( 'NONE', *, *, #14817, .T. ) ;
#662=EDGE_CURVE ( 'NONE', #12922, #16401, #2973, .T. ) ;
#687=LINE ( 'NONE', #17603, #4352 ) ;
#701=EDGE_CURVE ( 'NONE', #5888, #1832, #17295, .T. ) ;
#713=CARTESIAN_POINT ( 'NONE',  ( 0.5000000000000000000, 4.631370849898480024, 6.100000000000000533 ) ) ;
#718=EDGE_LOOP ( 'NONE', ( #2340, #1566, #11515, #12930 ) ) ;
#720=CARTESIAN_POINT ( 'NONE',  ( -1.399999999999999911, -9.500000000000000000, 3.299999999999999822 ) ) ;
#729=EDGE_LOOP ( 'NONE', ( #8849, #12695, #15570, #11829, #11114, #5194 ) ) ;
#730=ORIENTED_EDGE ( 'NONE', *, *, #9132, .F. ) ;
#736=PLANE ( 'NONE',  #17898 ) ;
#740=CARTESIAN_POINT ( 'NONE',  ( -1.800000000000000044, 0.5999999999999999778, 1.600000000000000089 ) ) ;
#750=ORIENTED_EDGE ( 'NONE', *, *, #6537, .T. ) ;
#755=CARTESIAN_POINT ( 'NONE',  ( 1.800000000000000044, 0.5999999999999999778, 7.599999999999999645 ) ) ;
#768=LINE ( 'NONE', #17692, #2401 ) ;
#770=VECTOR ( 'NONE', #4515, 1000.000000000000000 ) ;
#781=FACE_OUTER_BOUND ( 'NONE', #12825, .T. ) ;
#786=VERTEX_POINT ( 'NONE', #7488 ) ;
#788=LINE ( 'NONE', #12185, #4394 ) ;
#793=VECTOR ( 'NONE', #16639, 1000.000000000000000 ) ;
#797=LINE ( 'NONE', #17727, #12065 ) ;
#798=CARTESIAN_POINT ( 'NONE',  ( -1.399999999999999911, -7.000000000000000000, 3.299999999999999822 ) ) ;
#813=ADVANCED_FACE ( 'NONE', ( #14435 ), #10252, .T. ) ;
#816=ORIENTED_EDGE ( 'NONE', *, *, #17509, .T. ) ;
#817=AXIS2_PLACEMENT_3D ( 'NONE', #12785, #1981, #10411 ) ;
#823=LINE ( 'NONE', #6464, #13603 ) ;
#824=EDGE_LOOP ( 'NONE', ( #15107, #16470, #568, #13760, #3592, #3599, #8119, #9168, #15975 ) ) ;
#825=ORIENTED_EDGE ( 'NONE', *, *, #18216, .F. ) ;
#847=AXIS2_PLACEMENT_3D ( 'NONE', #1522, #3164, #11588 ) ;
#851=VERTEX_POINT ( 'NONE', #541 ) ;
#856=VECTOR ( 'NONE', #9398, 1000.000000000000000 ) ;
#858=VECTOR ( 'NONE', #4451, 1000.000000000000000 ) ;
#881=EDGE_CURVE ( 'NONE', #458, #14474, #12272, .T. ) ;
#897=CARTESIAN_POINT ( 'NONE',  ( -1.399999999999999911, -9.500000000000000000, 6.100000000000000533 ) ) ;
#902=CARTESIAN_POINT ( 'NONE',  ( 8.549934884138839976E-16, 6.262741699796950279, 6.100000000000000533 ) ) ;
#919=DIRECTION ( 'NONE',  ( -1.000000000000000000, 0.000000000000000000, 0.000000000000000000 ) ) ;
#925=DIRECTION ( 'NONE',  ( -1.000000000000000000, 0.000000000000000000, 0.000000000000000000 ) ) ;
#936=CARTESIAN_POINT ( 'NONE',  ( 0.5000000000000000000, 4.631370849898480024, 5.100000000000000533 ) ) ;
#957=VECTOR ( 'NONE', #14005, 1000.000000000000000 ) ;
#978=CARTESIAN_POINT ( 'NONE',  ( -1.399999999999999911, -5.500000000000000000, 6.100000000000000533 ) ) ;
#987=ORIENTED_EDGE ( 'NONE', *, *, #1836, .T. ) ;
#989=CARTESIAN_POINT ( 'NONE',  ( -1.399999999999999911, -8.000000000000000000, 3.299999999999999822 ) ) ;
#992=ORIENTED_EDGE ( 'NONE', *, *, #2120, .F. ) ;
#999=CARTESIAN_POINT ( 'NONE',  ( 0.4000000000000000222, -1.399999999999999911, 6.100000000000000533 ) ) ;
#1003=ORIENTED_EDGE ( 'NONE', *, *, #5108, .T. ) ;
#1016=CARTESIAN_POINT ( 'NONE',  ( 0.5500000000000000444, 7.799999999999999822, 3.600000000000000089 ) ) ;
#1039=VERTEX_POINT ( 'NONE', #11061 ) ;
#1063=CARTESIAN_POINT ( 'NONE',  ( 7.233457020361919865E-16, 4.000000000000000000, 6.100000000000000533 ) ) ;
#1066=PRODUCT ( 'Plunger Actuator', 'Plunger Actuator', '', ( #10668 ) ) ;
#1087=PLANE ( 'NONE',  #9686 ) ;
#1093=CARTESIAN_POINT ( 'NONE',  ( -1.399999999999999911, -5.000000000000000000, 3.299999999999999822 ) ) ;
#1097=DIRECTION ( 'NONE',  ( -1.899065700016719806E-16, -1.000000000000000000, 0.000000000000000000 ) ) ;
#1110=ADVANCED_FACE ( 'NONE', ( #13938 ), #2743, .F. ) ;
#1113=CARTESIAN_POINT ( 'NONE',  ( -1.000000000000000000, -7.000000000000000000, 3.700000000000000178 ) ) ;
#1137=CARTESIAN_POINT ( 'NONE',  ( -1.250000000000000000, 3.500000000000000000, 5.100000000000000533 ) ) ;
#1140=LINE ( 'NONE', #13645, #6405 ) ;
#1145=EDGE_LOOP ( 'NONE', ( #14306, #2927, #14326, #11786 ) ) ;
#1154=EDGE_CURVE ( 'NONE', #16167, #11049, #10982, .T. ) ;
#1159=CARTESIAN_POINT ( 'NONE',  ( 0.4000000000000000222, -1.399999999999999911, 5.100000000000000533 ) ) ;
#1161=DIRECTION ( 'NONE',  ( 2.220446049250319983E-16, 0.000000000000000000, 1.000000000000000000 ) ) ;
#1165=ORIENTED_EDGE ( 'NONE', *, *, #5182, .F. ) ;
#1170=FACE_OUTER_BOUND ( 'NONE', #7408, .T. ) ;
#1176=VECTOR ( 'NONE', #7596, 1000.000000000000000 ) ;
#1177=LINE ( 'NONE', #9309, #793 ) ;
#1184=DIRECTION ( 'NONE',  ( 7.930164461608269807E-17, 0.000000000000000000, 1.000000000000000000 ) ) ;
#1187=CARTESIAN_POINT ( 'NONE',  ( -0.9000000000000000222, 6.450000000000000178, 1.600000000000000089 ) ) ;
#1197=FACE_OUTER_BOUND ( 'NONE', #10533, .T. ) ;
#1204=CARTESIAN_POINT ( 'NONE',  ( 1.800000000000000044, 0.5999999999999999778, 1.600000000000000089 ) ) ;
#1212=ORIENTED_EDGE ( 'NONE', *, *, #177, .F. ) ;
#1224=LINE ( 'NONE', #9917, #13232 ) ;
#1226=PLANE ( 'NONE',  #11118 ) ;
#1232=ORIENTED_EDGE ( 'NONE', *, *, #3465, .T. ) ;
#1236=EDGE_CURVE ( 'NONE', #9612, #14617, #12910, .T. ) ;
#1253=EDGE_LOOP ( 'NONE', ( #13255, #13253, #16458, #2501, #11937, #987, #6096, #17907, #4300, #6844, #7260, #3756, #14489, #3680 ) ) ;
#1257=AXIS2_PLACEMENT_3D ( 'NONE', #1204, #11100, #6852 ) ;
#1266=EDGE_CURVE ( 'NONE', #8350, #17672, #4473, .T. ) ;
#1272=CARTESIAN_POINT ( 'NONE',  ( 1.800000000000000044, 7.799999999999999822, 7.599999999999999645 ) ) ;
#1274=VECTOR ( 'NONE', #1642, 1000.000000000000000 ) ;
#1277=DIRECTION ( 'NONE',  ( 1.000000000000000000, 0.000000000000000000, 6.344131569286600069E-16 ) ) ;
#1287=FACE_OUTER_BOUND ( 'NONE', #9651, .T. ) ;
#1290=LINE ( 'NONE', #13886, #16791 ) ;
#1299=CARTESIAN_POINT ( 'NONE',  ( 0.5000000000000000000, 5.762741699796949391, 5.100000000000000533 ) ) ;
#1305=DIRECTION ( 'NONE',  ( -1.746418240983389920E-16, 1.000000000000000000, 0.000000000000000000 ) ) ;
#1327=ORIENTED_EDGE ( 'NONE', *, *, #6740, .F. ) ;
#1329=DIRECTION ( 'NONE',  ( 1.000000000000000000, 0.000000000000000000, 0.000000000000000000 ) ) ;
#1331=VERTEX_POINT ( 'NONE', #15270 ) ;
#1344=CARTESIAN_POINT ( 'NONE',  ( 0.5000000000000000000, 3.500000000000000000, 5.100000000000000533 ) ) ;
#1348=PLANE ( 'NONE',  #12446 ) ;
#1349=CARTESIAN_POINT ( 'NONE',  ( 1.000000000000000000, -5.000000000000000000, 6.100000000000000533 ) ) ;
#1363=DIRECTION ( 'NONE',  ( 2.220446049250309876E-16, -1.000000000000000000, 0.000000000000000000 ) ) ;
#1366=PRODUCT_DEFINITION_SHAPE ( 'NONE', 'NONE',  #3578 ) ;
#1367=VERTEX_POINT ( 'NONE', #5164 ) ;
#1370=VECTOR ( 'NONE', #15490, 1000.000000000000000 ) ;
#1371=VERTEX_POINT ( 'NONE', #2492 ) ;
#1377=FACE_OUTER_BOUND ( 'NONE', #4552, .T. ) ;
#1386=VECTOR ( 'NONE', #9240, 1000.000000000000000 ) ;
#1392=CARTESIAN_POINT ( 'NONE',  ( 0.9000000000000000222, 2.050000000000000266, 3.600000000000000089 ) ) ;
#1394=FACE_OUTER_BOUND ( 'NONE', #824, .T. ) ;
#1397=EDGE_LOOP ( 'NONE', ( #10356, #9287, #15350, #6015 ) ) ;
#1405=VECTOR ( 'NONE', #14615, 1000.000000000000000 ) ;
#1409=VECTOR ( 'NONE', #12608, 1000.000000000000000 ) ;
#1423=FACE_OUTER_BOUND ( 'NONE', #2648, .T. ) ;
#1434=LINE ( 'NONE', #6706, #13508 ) ;
#1441=VECTOR ( 'NONE', #15725, 1000.000000000000000 ) ;
#1442=DIRECTION ( 'NONE',  ( 1.224646799147350002E-16, -1.000000000000000000, -6.123233995736769734E-17 ) ) ;
#1455=EDGE_CURVE ( 'NONE', #6816, #5243, #6923, .T. ) ;
#1463=VERTEX_POINT ( 'NONE', #11455 ) ;
#1469=LINE ( 'NONE', #2766, #17211 ) ;
#1470=LINE ( 'NONE', #7205, #4136 ) ;
#1479=VERTEX_POINT ( 'NONE', #15647 ) ;
#1488=PLANE ( 'NONE',  #2548 ) ;
#1493=LINE ( 'NONE', #4342, #15096 ) ;
#1500=DIRECTION ( 'NONE',  ( -1.480297366166879989E-16, 0.000000000000000000, 1.000000000000000000 ) ) ;
#1504=PLANE ( 'NONE',  #16196 ) ;
#1505=DIRECTION ( 'NONE',  ( 1.000000000000000000, 0.000000000000000000, 0.000000000000000000 ) ) ;
#1506=DIRECTION ( 'NONE',  ( 0.000000000000000000, -1.000000000000000000, -1.233581138472399909E-16 ) ) ;
#1515=DIRECTION ( 'NONE',  ( -1.189524669241239855E-16, 1.000000000000000000, 0.000000000000000000 ) ) ;
#1522=CARTESIAN_POINT ( 'NONE',  ( -4.687608326195109447E-16, -2.220446049250309876E-16, 3.600000000000000089 ) ) ;
#1528=VERTEX_POINT ( 'NONE', #2672 ) ;
#1529=ADVANCED_FACE ( 'NONE', ( #4417 ), #4140, .T. ) ;
#1535=DIRECTION ( 'NONE',  ( -1.480297366166879989E-16, -7.401486830834378990E-17, 1.000000000000000000 ) ) ;
#1536=ORIENTED_EDGE ( 'NONE', *, *, #2013, .F. ) ;
#1546=EDGE_CURVE ( 'NONE', #12743, #11049, #14241, .T. ) ;
#1547=ORIENTED_EDGE ( 'NONE', *, *, #6641, .T. ) ;
#1566=ORIENTED_EDGE ( 'NONE', *, *, #8695, .F. ) ;
#1573=EDGE_CURVE ( 'NONE', #5031, #13665, #1469, .T. ) ;
#1578=EDGE_CURVE ( 'NONE', #6801, #1039, #77, .T. ) ;
#1589=CARTESIAN_POINT ( 'NONE',  ( 6.735557395310439065E-16, -5.500000000000000000, -3.367778697655220026E-16 ) ) ;
#1600=DIRECTION ( 'NONE',  ( 1.593283298565159857E-16, -1.000000000000000000, -3.186566597130310346E-16 ) ) ;
#1605=CARTESIAN_POINT ( 'NONE',  ( -1.000000000000000000, -5.500000000000000000, 5.100000000000000533 ) ) ;
#1606=ORIENTED_EDGE ( 'NONE', *, *, #16883, .T. ) ;
#1619=CARTESIAN_POINT ( 'NONE',  ( -0.5500000000000000444, 6.450000000000000178, 3.600000000000000089 ) ) ;
#1627=LINE ( 'NONE', #4660, #6210 ) ;
#1631=CARTESIAN_POINT ( 'NONE',  ( -0.9000000000000000222, 2.050000000000000266, 3.600000000000000089 ) ) ;
#1642=DIRECTION ( 'NONE',  ( 1.000000000000000000, 0.000000000000000000, 0.000000000000000000 ) ) ;
#1653=DIRECTION ( 'NONE',  ( -1.000000000000000000, -1.233581138472399909E-16, -1.480297366166879989E-16 ) ) ;
#1657=CARTESIAN_POINT ( 'NONE',  ( -0.5500000000000000444, 6.450000000000000178, 1.600000000000000089 ) ) ;
#1678=CLOSED_SHELL ( 'NONE', ( #17250, #10957, #2235, #14129, #6811, #13216, #6897, #6200, #5319, #10041, #4520, #3704, #315, #105, #14666, #4593, #6660, #13195, #5516, #8926, #8648, #17271, #17198, #13006, #14621, #3585, #15481, #18027, #12510, #4723, #2807, #4042, #259, #18212, #2599, #5995, #17741, #11109, #16494, #11392, #3802, #17042, #12519, #13359, #813, #8455, #15528, #1529, #7562, #16316, #5674, #14159, #4712, #1990, #14350, #3991, #1110, #8864, #17976, #15869, #16128, #17491, #15822, #8789, #13718, #3819, #16655, #8044, #598, #16948, #7270, #8598 ) ) ;
#1705=ORIENTED_EDGE ( 'NONE', *, *, #7576, .T. ) ;
#1707=DIRECTION ( 'NONE',  ( -2.018587317500279868E-16, 1.000000000000000000, 0.000000000000000000 ) ) ;
#1711=CARTESIAN_POINT ( 'NONE',  ( 1.399999999999999911, -5.000000000000000000, 6.100000000000000533 ) ) ;
#1714=VECTOR ( 'NONE', #925, 1000.000000000000000 ) ;
#1747=AXIS2_PLACEMENT_3D ( 'NONE', #7958, #13604, #17827 ) ;
#1802=EDGE_CURVE ( 'NONE', #16922, #8308, #12441, .T. ) ;
#1804=CARTESIAN_POINT ( 'NONE',  ( -1.399999999999999911, -5.500000000000000000, 6.100000000000000533 ) ) ;
#1808=ORIENTED_EDGE ( 'NONE', *, *, #10536, .F. ) ;
#1811=EDGE_CURVE ( 'NONE', #12303, #13228, #11997, .T. ) ;
#1825=FACE_OUTER_BOUND ( 'NONE', #59, .T. ) ;
#1832=VERTEX_POINT ( 'NONE', #897 ) ;
#1836=EDGE_CURVE ( 'NONE', #12743, #12376, #17613, .T. ) ;
#1849=ORIENTED_EDGE ( 'NONE', *, *, #2013, .T. ) ;
#1850=CARTESIAN_POINT ( 'NONE',  ( -1.250000000000000000, 0.5999999999999999778, 7.599999999999999645 ) ) ;
#1852=CARTESIAN_POINT ( 'NONE',  ( -0.5500000000000000444, 2.050000000000000266, 1.600000000000000089 ) ) ;
#1865=ORIENTED_EDGE ( 'NONE', *, *, #11964, .F. ) ;
#1867=DIRECTION ( 'NONE',  ( -1.000000000000000000, 1.899065700016719806E-16, 0.000000000000000000 ) ) ;
#1875=VERTEX_POINT ( 'NONE', #5294 ) ;
#1894=EDGE_CURVE ( 'NONE', #10460, #6927, #4075, .T. ) ;
#1901=ORIENTED_EDGE ( 'NONE', *, *, #93, .T. ) ;
#1903=MANIFOLD_SOLID_BREP ( 'Stock-MAS-687-1', #1678 ) ;
#1927=DIRECTION ( 'NONE',  ( -1.000000000000000000, 0.000000000000000000, -6.344131569286600069E-16 ) ) ;
#1981=DIRECTION ( 'NONE',  ( -0.7071067811865480168, 0.7071067811865470176, 0.000000000000000000 ) ) ;
#1987=ORIENTED_EDGE ( 'NONE', *, *, #6543, .T. ) ;
#1990=ADVANCED_FACE ( 'NONE', ( #13051 ), #7315, .F. ) ;
#1991=DIRECTION ( 'NONE',  ( 0.000000000000000000, 6.123233995736769734E-17, -1.000000000000000000 ) ) ;
#2013=EDGE_CURVE ( 'NONE', #17672, #2905, #7229, .T. ) ;
#2021=CARTESIAN_POINT ( 'NONE',  ( -1.000000000000000000, -7.000000000000000000, 5.700000000000000178 ) ) ;
#2027=SHAPE_REPRESENTATION ( 'Plunger Actuator', ( #17681 ), #4992 ) ;
#2055=EDGE_CURVE ( 'NONE', #1463, #12743, #11934, .T. ) ;
#2056=AXIS2_PLACEMENT_3D ( 'NONE', #3679, #17643, #9526 ) ;
#2059=EDGE_CURVE ( 'NONE', #15231, #18019, #9238, .T. ) ;
#2079=AXIS2_PLACEMENT_3D ( 'NONE', #14225, #11436, #5709 ) ;
#2084=CARTESIAN_POINT ( 'NONE',  ( 1.399999999999999911, -8.000000000000000000, 6.100000000000000533 ) ) ;
#2086=LINE ( 'NONE', #8117, #14209 ) ;
#2087=EDGE_CURVE ( 'NONE', #13096, #15231, #5116, .T. ) ;
#2092=DIRECTION ( 'NONE',  ( 1.776356839400249824E-16, 3.552713678800500140E-16, -1.000000000000000000 ) ) ;
#2102=EDGE_CURVE ( 'NONE', #620, #13315, #17647, .T. ) ;
#2107=ORIENTED_EDGE ( 'NONE', *, *, #4843, .T. ) ;
#2118=FACE_OUTER_BOUND ( 'NONE', #11604, .T. ) ;
#2119=CARTESIAN_POINT ( 'NONE',  ( -0.9000000000000000222, 6.450000000000000178, 3.600000000000000089 ) ) ;
#2120=EDGE_CURVE ( 'NONE', #14390, #1331, #12027, .T. ) ;
#2128=EDGE_CURVE ( 'NONE', #11596, #17115, #13509, .T. ) ;
#2129=CARTESIAN_POINT ( 'NONE',  ( -1.399999999999999911, -8.000000000000000000, 3.299999999999999822 ) ) ;
#2136=CARTESIAN_POINT ( 'NONE',  ( -0.9000000000000000222, -10.00000000000000000, 6.100000000000000533 ) ) ;
#2142=ORIENTED_EDGE ( 'NONE', *, *, #3124, .F. ) ;
#2143=VECTOR ( 'NONE', #8191, 1000.000000000000000 ) ;
#2147=VERTEX_POINT ( 'NONE', #3501 ) ;
#2149=SHAPE_DEFINITION_REPRESENTATION ( #1366, #2027 ) ;
#2161=DIRECTION ( 'NONE',  ( 0.000000000000000000, 0.000000000000000000, -1.000000000000000000 ) ) ;
#2164=DIRECTION ( 'NONE',  ( 0.7071067811865470176, -0.7071067811865480168, 0.000000000000000000 ) ) ;
#2172=PLANE ( 'NONE',  #4005 ) ;
#2192=AXIS2_PLACEMENT_3D ( 'NONE', #7153, #102, #15751 ) ;
#2197=CARTESIAN_POINT ( 'NONE',  ( -1.000000000000000000, -7.000000000000000000, 3.700000000000000178 ) ) ;
#2210=LINE ( 'NONE', #14898, #16256 ) ;
#2217=ORIENTED_EDGE ( 'NONE', *, *, #8991, .T. ) ;
#2230=EDGE_CURVE ( 'NONE', #5300, #7556, #17927, .T. ) ;
#2235=ADVANCED_FACE ( 'NONE', ( #18105 ), #11008, .T. ) ;
#2260=DIRECTION ( 'NONE',  ( 0.000000000000000000, 0.000000000000000000, 1.000000000000000000 ) ) ;
#2266=DIRECTION ( 'NONE',  ( 2.467162276944790449E-16, 0.000000000000000000, 1.000000000000000000 ) ) ;
#2272=EDGE_CURVE ( 'NONE', #7510, #3530, #2337, .T. ) ;
#2274=AXIS2_PLACEMENT_3D ( 'NONE', #13510, #16289, #3503 ) ;
#2278=ORIENTED_EDGE ( 'NONE', *, *, #11315, .F. ) ;
#2284=ORIENTED_EDGE ( 'NONE', *, *, #2467, .F. ) ;
#2297=VECTOR ( 'NONE', #2349, 1000.000000000000000 ) ;
#2307=PLANE ( 'NONE',  #1747 ) ;
#2320=ORIENTED_EDGE ( 'NONE', *, *, #10377, .T. ) ;
#2324=FACE_OUTER_BOUND ( 'NONE', #5273, .T. ) ;
#2335=VERTEX_POINT ( 'NONE', #16397 ) ;
#2337=LINE ( 'NONE', #6581, #17545 ) ;
#2340=ORIENTED_EDGE ( 'NONE', *, *, #14430, .F. ) ;
#2349=DIRECTION ( 'NONE',  ( 1.000000000000000000, 0.000000000000000000, 0.000000000000000000 ) ) ;
#2365=VECTOR ( 'NONE', #14263, 1000.000000000000000 ) ;
#2371=EDGE_CURVE ( 'NONE', #6313, #3213, #6671, .T. ) ;
#2378=CARTESIAN_POINT ( 'NONE',  ( -1.399999999999999911, 0.5999999999999999778, 6.100000000000000533 ) ) ;
#2394=ORIENTED_EDGE ( 'NONE', *, *, #13617, .T. ) ;
#2400=CARTESIAN_POINT ( 'NONE',  ( -0.5500000000000000444, 0.5999999999999999778, 3.299999999999999822 ) ) ;
#2401=VECTOR ( 'NONE', #5025, 1000.000000000000000 ) ;
#2406=ORIENTED_EDGE ( 'NONE', *, *, #15210, .F. ) ;
#2413=VERTEX_POINT ( 'NONE', #7984 ) ;
#2417=PLANE ( 'NONE',  #9639 ) ;
#2423=LINE ( 'NONE', #3790, #255 ) ;
#2425=DIRECTION ( 'NONE',  ( 2.960594732333750117E-16, -1.000000000000000000, 0.000000000000000000 ) ) ;
#2456=PLANE ( 'NONE',  #7861 ) ;
#2460=DIRECTION ( 'NONE',  ( -1.306144734853129823E-16, -6.530723674265629391E-17, 1.000000000000000000 ) ) ;
#2463=LINE ( 'NONE', #5226, #13825 ) ;
#2467=EDGE_CURVE ( 'NONE', #16167, #4320, #12419, .T. ) ;
#2473=ORIENTED_EDGE ( 'NONE', *, *, #9614, .T. ) ;
#2478=PLANE ( 'NONE',  #6394 ) ;
#2480=EDGE_LOOP ( 'NONE', ( #6075, #9587, #4860, #5883 ) ) ;
#2492=CARTESIAN_POINT ( 'NONE',  ( -0.9000000000000000222, 2.050000000000000266, 1.600000000000000089 ) ) ;
#2500=DIRECTION ( 'NONE',  ( 1.000000000000000000, -1.608122649676639805E-16, 0.000000000000000000 ) ) ;
#2501=ORIENTED_EDGE ( 'NONE', *, *, #9432, .T. ) ;
#2519=LINE ( 'NONE', #18218, #5371 ) ;
#2531=CARTESIAN_POINT ( 'NONE',  ( 0.4000000000000000222, 2.399999999999999911, 6.100000000000000533 ) ) ;
#2536=CARTESIAN_POINT ( 'NONE',  ( 0.000000000000000000, 0.000000000000000000, 5.100000000000000533 ) ) ;
#2539=CARTESIAN_POINT ( 'NONE',  ( 0.9000000000000000222, 2.050000000000000266, 3.600000000000000089 ) ) ;
#2540=LINE ( 'NONE', #12455, #14185 ) ;
#2542=DIRECTION ( 'NONE',  ( 0.000000000000000000, 0.000000000000000000, 1.000000000000000000 ) ) ;
#2548=AXIS2_PLACEMENT_3D ( 'NONE', #5823, #12864, #7222 ) ;
#2550=ORIENTED_EDGE ( 'NONE', *, *, #16540, .F. ) ;
#2555=FACE_OUTER_BOUND ( 'NONE', #7880, .T. ) ;
#2576=DIRECTION ( 'NONE',  ( -1.224646799147350002E-16, 1.000000000000000000, 6.123233995736769734E-17 ) ) ;
#2578=ORIENTED_EDGE ( 'NONE', *, *, #12979, .T. ) ;
#2580=DIRECTION ( 'NONE',  ( 1.000000000000000000, 0.000000000000000000, 0.000000000000000000 ) ) ;
#2585=AXIS2_PLACEMENT_3D ( 'NONE', #5428, #11065, #16709 ) ;
#2587=AXIS2_PLACEMENT_3D ( 'NONE', #13605, #8055, #919 ) ;
#2588=VECTOR ( 'NONE', #6221, 1000.000000000000000 ) ;
#2593=CARTESIAN_POINT ( 'NONE',  ( -1.250000000000000000, 3.881370849898470254, 6.100000000000000533 ) ) ;
#2599=ADVANCED_FACE ( 'NONE', ( #7762 ), #3587, .F. ) ;
#2612=VECTOR ( 'NONE', #15081, 1000.000000000000000 ) ;
#2614=PLANE ( 'NONE',  #17676 ) ;
#2623=DIRECTION ( 'NONE',  ( -1.448116988641510032E-16, 0.000000000000000000, -1.000000000000000000 ) ) ;
#2641=ORIENTED_EDGE ( 'NONE', *, *, #2055, .F. ) ;
#2648=EDGE_LOOP ( 'NONE', ( #15532, #11027, #15752, #1547, #13535, #7723, #5120, #8060, #15565, #11358, #12001, #12405 ) ) ;
#2666=VECTOR ( 'NONE', #11388, 1000.000000000000000 ) ;
#2672=CARTESIAN_POINT ( 'NONE',  ( -0.5500000000000000444, -2.399999999999999911, 3.299999999999999822 ) ) ;
#2677=ORIENTED_EDGE ( 'NONE', *, *, #10536, .T. ) ;
#2681=VERTEX_POINT ( 'NONE', #4737 ) ;
#2693=LINE ( 'NONE', #17021, #2666 ) ;
#2694=VERTEX_POINT ( 'NONE', #16048 ) ;
#2704=LINE ( 'NONE', #12427, #12086 ) ;
#2714=LINE ( 'NONE', #28, #1370 ) ;
#2743=PLANE ( 'NONE',  #88 ) ;
#2766=CARTESIAN_POINT ( 'NONE',  ( -1.000000000000000000, -5.500000000000000000, 5.100000000000000533 ) ) ;
#2778=LINE ( 'NONE', #9717, #151 ) ;
#2779=CARTESIAN_POINT ( 'NONE',  ( 0.9000000000000000222, -9.500000000000000000, 6.100000000000000533 ) ) ;
#2785=VERTEX_POINT ( 'NONE', #6679 ) ;
#2793=DIRECTION ( 'NONE',  ( -2.018587317500279868E-16, 1.000000000000000000, 1.009293658750139934E-16 ) ) ;
#2800=CARTESIAN_POINT ( 'NONE',  ( -1.250000000000000000, 0.5999999999999999778, 7.599999999999999645 ) ) ;
#2805=VERTEX_POINT ( 'NONE', #3815 ) ;
#2807=ADVANCED_FACE ( 'NONE', ( #13444 ), #5305, .T. ) ;
#2814=CARTESIAN_POINT ( 'NONE',  ( 0.5000000000000000000, 4.631370849898480024, 5.100000000000000533 ) ) ;
#2818=ORIENTED_EDGE ( 'NONE', *, *, #8134, .T. ) ;
#2821=ORIENTED_EDGE ( 'NONE', *, *, #662, .T. ) ;
#2830=FACE_OUTER_BOUND ( 'NONE', #17027, .T. ) ;
#2838=DIRECTION ( 'NONE',  ( 1.110223024625159992E-16, 0.000000000000000000, -1.000000000000000000 ) ) ;
#2846=ORIENTED_EDGE ( 'NONE', *, *, #1578, .F. ) ;
#2870=DIRECTION ( 'NONE',  ( -1.480297366166879989E-16, 1.000000000000000000, 1.480297366166879989E-16 ) ) ;
#2878=VERTEX_POINT ( 'NONE', #12062 ) ;
#2896=DIRECTION ( 'NONE',  ( 2.220446049250309876E-16, 2.960594732333750117E-16, -1.000000000000000000 ) ) ;
#2900=AXIS2_PLACEMENT_3D ( 'NONE', #8717, #7508, #1515 ) ;
#2905=VERTEX_POINT ( 'NONE', #15313 ) ;
#2922=DIRECTION ( 'NONE',  ( -1.644774851296529842E-16, 1.000000000000000000, 0.000000000000000000 ) ) ;
#2927=ORIENTED_EDGE ( 'NONE', *, *, #8577, .F. ) ;
#2931=ORIENTED_EDGE ( 'NONE', *, *, #15210, .T. ) ;
#2939=EDGE_CURVE ( 'NONE', #9877, #17390, #15131, .T. ) ;
#2952=VECTOR ( 'NONE', #13895, 1000.000000000000000 ) ;
#2957=ORIENTED_EDGE ( 'NONE', *, *, #10065, .T. ) ;
#2958=EDGE_CURVE ( 'NONE', #8588, #2335, #16408, .T. ) ;
#2959=ORIENTED_EDGE ( 'NONE', *, *, #18057, .T. ) ;
#2973=LINE ( 'NONE', #13974, #9031 ) ;
#2975=EDGE_CURVE ( 'NONE', #5888, #15231, #1140, .T. ) ;
#2986=CARTESIAN_POINT ( 'NONE',  ( -5.045174592681759329E-16, -1.399999999999999911, 5.100000000000000533 ) ) ;
#2989=CARTESIAN_POINT ( 'NONE',  ( 6.429395695523600208E-16, 3.500000000000000000, 6.100000000000000533 ) ) ;
#2998=ORIENTED_EDGE ( 'NONE', *, *, #1154, .T. ) ;
#3002=ORIENTED_EDGE ( 'NONE', *, *, #2939, .F. ) ;
#3018=DIRECTION ( 'NONE',  ( -1.000000000000000000, 0.000000000000000000, 0.000000000000000000 ) ) ;
#3029=DIRECTION ( 'NONE',  ( 1.000000000000000000, 0.000000000000000000, 0.000000000000000000 ) ) ;
#3048=FACE_OUTER_BOUND ( 'NONE', #2480, .T. ) ;
#3066=CARTESIAN_POINT ( 'NONE',  ( 1.250000000000000000, 7.799999999999999822, 6.100000000000000533 ) ) ;
#3095=ORIENTED_EDGE ( 'NONE', *, *, #7669, .F. ) ;
#3109=CARTESIAN_POINT ( 'NONE',  ( 8.572527594031470232E-16, -7.000000000000000000, -4.286263797015740046E-16 ) ) ;
#3115=ORIENTED_EDGE ( 'NONE', *, *, #11653, .F. ) ;
#3124=EDGE_CURVE ( 'NONE', #9612, #786, #7242, .T. ) ;
#3144=EDGE_CURVE ( 'NONE', #11596, #8415, #4450, .T. ) ;
#3148=DIRECTION ( 'NONE',  ( 1.000000000000000000, 0.000000000000000000, 0.000000000000000000 ) ) ;
#3158=ORIENTED_EDGE ( 'NONE', *, *, #5156, .F. ) ;
#3162=ORIENTED_EDGE ( 'NONE', *, *, #4278, .T. ) ;
#3164=DIRECTION ( 'NONE',  ( 1.233581138472399909E-16, 6.167905692361979821E-17, -1.000000000000000000 ) ) ;
#3166=ORIENTED_EDGE ( 'NONE', *, *, #15506, .F. ) ;
#3203=AXIS2_PLACEMENT_3D ( 'NONE', #4707, #10928, #13882 ) ;
#3205=CARTESIAN_POINT ( 'NONE',  ( 0.5000000000000000000, 4.631370849898480024, 5.100000000000000533 ) ) ;
#3213=VERTEX_POINT ( 'NONE', #10109 ) ;
#3216=SHAPE_REPRESENTATION_RELATIONSHIP ( 'NONE' , 'NONE' ,  #2027, #3778 ) ;
#3224=DIRECTION ( 'NONE',  ( 1.000000000000000000, 4.037174635000579950E-16, 0.000000000000000000 ) ) ;
#3230=VECTOR ( 'NONE', #8812, 1000.000000000000000 ) ;
#3239=PLANE ( 'NONE',  #5548 ) ;
#3255=EDGE_LOOP ( 'NONE', ( #11108, #6254, #9730, #5011 ) ) ;
#3269=DIRECTION ( 'NONE',  ( 1.000000000000000000, 0.000000000000000000, 0.000000000000000000 ) ) ;
#3274=FACE_OUTER_BOUND ( 'NONE', #17645, .T. ) ;
#3277=LINE ( 'NONE', #17421, #15616 ) ;
#3279=ORIENTED_EDGE ( 'NONE', *, *, #436, .F. ) ;
#3281=EDGE_CURVE ( 'NONE', #6472, #17115, #15846, .T. ) ;
#3282=EDGE_LOOP ( 'NONE', ( #16106, #17648, #5702, #12208 ) ) ;
#3298=CARTESIAN_POINT ( 'NONE',  ( 1.250000000000000000, 6.144112549695430303, 6.100000000000000533 ) ) ;
#3313=PLANE ( 'NONE',  #6424 ) ;
#3342=ORIENTED_EDGE ( 'NONE', *, *, #10583, .T. ) ;
#3362=( GEOMETRIC_REPRESENTATION_CONTEXT ( 3 ) GLOBAL_UNCERTAINTY_ASSIGNED_CONTEXT ( ( #8082 ) ) GLOBAL_UNIT_ASSIGNED_CONTEXT ( ( #4521, #11213, #15569 ) ) REPRESENTATION_CONTEXT ( 'NONE', 'WORKASPACE' ) );
#3377=LINE ( 'NONE', #11721, #14787 ) ;
#3388=CARTESIAN_POINT ( 'NONE',  ( 1.250000000000000000, 0.5999999999999999778, 7.599999999999999645 ) ) ;
#3412=LINE ( 'NONE', #16393, #531 ) ;
#3419=ORIENTED_EDGE ( 'NONE', *, *, #9432, .F. ) ;
#3424=VECTOR ( 'NONE', #2460, 1000.000000000000000 ) ;
#3440=CARTESIAN_POINT ( 'NONE',  ( 1.250000000000000000, 6.144112549695430303, 5.100000000000000533 ) ) ;
#3465=EDGE_CURVE ( 'NONE', #7904, #620, #3851, .T. ) ;
#3468=EDGE_LOOP ( 'NONE', ( #13484, #13630, #2931, #9071 ) ) ;
#3470=VECTOR ( 'NONE', #9500, 1000.000000000000000 ) ;
#3477=EDGE_CURVE ( 'NONE', #5262, #3744, #16257, .T. ) ;
#3487=AXIS2_PLACEMENT_3D ( 'NONE', #17306, #477, #4904 ) ;
#3493=VECTOR ( 'NONE', #13772, 1000.000000000000000 ) ;
#3496=AXIS2_PLACEMENT_3D ( 'NONE', #21, #11484, #1500 ) ;
#3499=EDGE_LOOP ( 'NONE', ( #8353, #5809, #12333, #11809 ) ) ;
#3501=CARTESIAN_POINT ( 'NONE',  ( -0.4000000000000000222, 2.399999999999999911, 6.100000000000000533 ) ) ;
#3503=DIRECTION ( 'NONE',  ( -2.379049338482479710E-16, 0.000000000000000000, -1.000000000000000000 ) ) ;
#3516=DIRECTION ( 'NONE',  ( -1.110223024625159992E-16, 0.000000000000000000, 1.000000000000000000 ) ) ;
#3522=ORIENTED_EDGE ( 'NONE', *, *, #3477, .F. ) ;
#3523=VECTOR ( 'NONE', #6288, 1000.000000000000000 ) ;
#3530=VERTEX_POINT ( 'NONE', #7933 ) ;
#3539=VERTEX_POINT ( 'NONE', #9959 ) ;
#3554=ORIENTED_EDGE ( 'NONE', *, *, #16644, .F. ) ;
#3560=DIRECTION ( 'NONE',  ( -1.000000000000000000, 0.000000000000000000, 0.000000000000000000 ) ) ;
#3568=DIRECTION ( 'NONE',  ( 1.110223024625159992E-16, 4.440892098500630106E-16, -1.000000000000000000 ) ) ;
#3578=PRODUCT_DEFINITION ( 'UNKNOWN', '', #15377, #6775 ) ;
#3585=ADVANCED_FACE ( 'NONE', ( #1170 ), #6818, .F. ) ;
#3587=CYLINDRICAL_SURFACE ( 'NONE', #2587, 0.4000000000000000222 ) ;
#3592=ORIENTED_EDGE ( 'NONE', *, *, #1546, .T. ) ;
#3593=CARTESIAN_POINT ( 'NONE',  ( -0.9000000000000000222, 6.450000000000000178, 1.600000000000000089 ) ) ;
#3599=ORIENTED_EDGE ( 'NONE', *, *, #4595, .T. ) ;
#3616=DIRECTION ( 'NONE',  ( -1.899065700016719806E-16, -1.000000000000000000, 0.000000000000000000 ) ) ;
#3627=ORIENTED_EDGE ( 'NONE', *, *, #1455, .T. ) ;
#3657=LINE ( 'NONE', #5147, #4736 ) ;
#3661=EDGE_LOOP ( 'NONE', ( #4569, #11417, #3419, #15550 ) ) ;
#3665=CARTESIAN_POINT ( 'NONE',  ( -1.000000000000000000, -7.000000000000000000, 3.700000000000000178 ) ) ;
#3675=FACE_OUTER_BOUND ( 'NONE', #13560, .T. ) ;
#3679=CARTESIAN_POINT ( 'NONE',  ( -0.9000000000000000222, -9.500000000000000000, 8.099999999999999645 ) ) ;
#3680=ORIENTED_EDGE ( 'NONE', *, *, #8960, .T. ) ;
#3684=LINE ( 'NONE', #1852, #1405 ) ;
#3685=CARTESIAN_POINT ( 'NONE',  ( -1.399999999999999911, -9.500000000000000000, 3.299999999999999822 ) ) ;
#3688=EDGE_CURVE ( 'NONE', #14447, #2805, #8881, .T. ) ;
#3690=CARTESIAN_POINT ( 'NONE',  ( 2.220446049250309876E-16, 2.399999999999999911, 6.100000000000000533 ) ) ;
#3704=ADVANCED_FACE ( 'NONE', ( #15930 ), #3239, .F. ) ;
#3716=VERTEX_POINT ( 'NONE', #16024 ) ;
#3722=EDGE_CURVE ( 'NONE', #1331, #5830, #7677, .T. ) ;
#3728=DIRECTION ( 'NONE',  ( 1.000000000000000000, 0.000000000000000000, 0.000000000000000000 ) ) ;
#3731=CARTESIAN_POINT ( 'NONE',  ( 1.000000000000000000, -5.000000000000000000, 3.299999999999999822 ) ) ;
#3744=VERTEX_POINT ( 'NONE', #14531 ) ;
#3752=ORIENTED_EDGE ( 'NONE', *, *, #10639, .F. ) ;
#3755=CARTESIAN_POINT ( 'NONE',  ( -1.000000000000000000, -5.500000000000000000, 6.100000000000000533 ) ) ;
#3756=ORIENTED_EDGE ( 'NONE', *, *, #8364, .T. ) ;
#3778=ADVANCED_BREP_SHAPE_REPRESENTATION ( '', ( #1903, #17681 ), #4992 ) ;
#3786=VECTOR ( 'NONE', #15237, 1000.000000000000000 ) ;
#3790=CARTESIAN_POINT ( 'NONE',  ( 1.800000000000000044, 7.799999999999999822, 1.600000000000000089 ) ) ;
#3802=ADVANCED_FACE ( 'NONE', ( #2118 ), #6193, .T. ) ;
#3807=CARTESIAN_POINT ( 'NONE',  ( -0.5500000000000000444, 2.050000000000000266, 3.600000000000000089 ) ) ;
#3815=CARTESIAN_POINT ( 'NONE',  ( -1.399999999999999911, 0.5999999999999999778, 3.299999999999999822 ) ) ;
#3819=ADVANCED_FACE ( 'NONE', ( #10733 ), #11849, .F. ) ;
#3843=EDGE_CURVE ( 'NONE', #12574, #14329, #6363, .T. ) ;
#3851=LINE ( 'NONE', #7828, #4055 ) ;
#3866=EDGE_CURVE ( 'NONE', #1371, #14390, #3684, .T. ) ;
#3889=CARTESIAN_POINT ( 'NONE',  ( 0.9000000000000000222, -10.00000000000000000, 6.100000000000000533 ) ) ;
#3902=DIRECTION ( 'NONE',  ( 0.000000000000000000, 0.000000000000000000, -1.000000000000000000 ) ) ;
#3937=EDGE_CURVE ( 'NONE', #9952, #7556, #7968, .T. ) ;
#3952=FACE_OUTER_BOUND ( 'NONE', #15929, .T. ) ;
#3960=DIRECTION ( 'NONE',  ( 1.000000000000000000, 0.000000000000000000, 0.000000000000000000 ) ) ;
#3962=ORIENTED_EDGE ( 'NONE', *, *, #13676, .F. ) ;
#3963=ORIENTED_EDGE ( 'NONE', *, *, #7236, .F. ) ;
#3967=ORIENTED_EDGE ( 'NONE', *, *, #10369, .F. ) ;
#3970=DIRECTION ( 'NONE',  ( -1.257750167763089819E-32, 7.930164461608259947E-17, -1.000000000000000000 ) ) ;
#3983=UNCERTAINTY_MEASURE_WITH_UNIT (LENGTH_MEASURE( 1.000000000000000082E-05 ), #14596, 'distance_accuracy_value', 'NONE');
#3991=ADVANCED_FACE ( 'NONE', ( #1197 ), #2417, .F. ) ;
#3992=CARTESIAN_POINT ( 'NONE',  ( -1.000000000000000000, -7.000000000000000000, 3.700000000000000178 ) ) ;
#4005=AXIS2_PLACEMENT_3D ( 'NONE', #6605, #10972, #3728 ) ;
#4029=ORIENTED_EDGE ( 'NONE', *, *, #13500, .T. ) ;
#4033=VECTOR ( 'NONE', #6680, 1000.000000000000000 ) ;
#4042=ADVANCED_FACE ( 'NONE', ( #9919 ), #1226, .T. ) ;
#4054=LINE ( 'NONE', #3685, #544 ) ;
#4055=VECTOR ( 'NONE', #15159, 1000.000000000000000 ) ;
#4056=ORIENTED_EDGE ( 'NONE', *, *, #7413, .F. ) ;
#4057=VECTOR ( 'NONE', #15488, 1000.000000000000000 ) ;
#4061=CARTESIAN_POINT ( 'NONE',  ( -1.250000000000000000, 3.500000000000000000, 5.100000000000000533 ) ) ;
#4075=LINE ( 'NONE', #3807, #11646 ) ;
#4076=ORIENTED_EDGE ( 'NONE', *, *, #10243, .F. ) ;
#4077=EDGE_LOOP ( 'NONE', ( #11234, #7732, #14892, #17804 ) ) ;
#4078=VECTOR ( 'NONE', #13750, 1000.000000000000000 ) ;
#4084=VECTOR ( 'NONE', #9231, 1000.000000000000000 ) ;
#4110=LINE ( 'NONE', #1159, #14078 ) ;
#4111=CARTESIAN_POINT ( 'NONE',  ( 1.399999999999998579, -9.792893218813446765, 3.300000000000000266 ) ) ;
#4117=CARTESIAN_POINT ( 'NONE',  ( 7.347880794884119736E-16, -6.000000000000000000, -3.673940397442060361E-16 ) ) ;
#4123=ORIENTED_EDGE ( 'NONE', *, *, #17038, .T. ) ;
#4132=CARTESIAN_POINT ( 'NONE',  ( 0.5500000000000000444, -2.399999999999999911, 3.600000000000000089 ) ) ;
#4136=VECTOR ( 'NONE', #11187, 1000.000000000000000 ) ;
#4140=PLANE ( 'NONE',  #14886 ) ;
#4146=DIRECTION ( 'NONE',  ( 1.000000000000000000, 0.000000000000000000, 0.000000000000000000 ) ) ;
#4163=ORIENTED_EDGE ( 'NONE', *, *, #8017, .F. ) ;
#4166=ORIENTED_EDGE ( 'NONE', *, *, #2059, .T. ) ;
#4202=VECTOR ( 'NONE', #17148, 1000.000000000000000 ) ;
#4217=ORIENTED_EDGE ( 'NONE', *, *, #1811, .T. ) ;
#4229=PLANE ( 'NONE',  #11529 ) ;
#4235=CARTESIAN_POINT ( 'NONE',  ( 1.399999999999999911, 0.5999999999999999778, 6.100000000000000533 ) ) ;
#4236=ORIENTED_EDGE ( 'NONE', *, *, #10102, .T. ) ;
#4239=PLANE ( 'NONE',  #13363 ) ;
#4254=FACE_OUTER_BOUND ( 'NONE', #18088, .T. ) ;
#4261=DIRECTION ( 'NONE',  ( -1.110223024625159992E-16, 0.000000000000000000, -1.000000000000000000 ) ) ;
#4263=LINE ( 'NONE', #15583, #7367 ) ;
#4278=EDGE_CURVE ( 'NONE', #3539, #138, #9054, .T. ) ;
#4279=EDGE_LOOP ( 'NONE', ( #9149, #15954, #3002, #15617 ) ) ;
#4283=EDGE_LOOP ( 'NONE', ( #9913, #5730, #13015, #18242, #5041, #8159, #7055, #1705, #18261, #8124, #13963, #1536, #17691, #6887, #14369, #10316, #8144, #2107, #9987 ) ) ;
#4295=CARTESIAN_POINT ( 'NONE',  ( 1.000000000000000000, -7.000000000000000000, 3.700000000000000178 ) ) ;
#4300=ORIENTED_EDGE ( 'NONE', *, *, #11315, .T. ) ;
#4308=FACE_OUTER_BOUND ( 'NONE', #718, .T. ) ;
#4312=ORIENTED_EDGE ( 'NONE', *, *, #13870, .F. ) ;
#4320=VERTEX_POINT ( 'NONE', #6204 ) ;
#4329=PLANE ( 'NONE',  #1257 ) ;
#4331=VECTOR ( 'NONE', #7224, 1000.000000000000000 ) ;
#4339=VECTOR ( 'NONE', #3224, 1000.000000000000000 ) ;
#4342=CARTESIAN_POINT ( 'NONE',  ( -1.399999999999999911, -6.000000000000000000, 3.299999999999999822 ) ) ;
#4346=DIRECTION ( 'NONE',  ( 1.224646799147350002E-16, -1.000000000000000000, -6.123233995736769734E-17 ) ) ;
#4348=EDGE_CURVE ( 'NONE', #1875, #10826, #15758, .T. ) ;
#4350=ORIENTED_EDGE ( 'NONE', *, *, #17509, .F. ) ;
#4352=VECTOR ( 'NONE', #10594, 1000.000000000000000 ) ;
#4364=VECTOR ( 'NONE', #2161, 1000.000000000000000 ) ;
#4372=FACE_OUTER_BOUND ( 'NONE', #3661, .T. ) ;
#4373=EDGE_LOOP ( 'NONE', ( #825, #7346, #9497, #5202 ) ) ;
#4387=CARTESIAN_POINT ( 'NONE',  ( 0.9000000000000000222, -10.00000000000000000, 3.799999999999999822 ) ) ;
#4394=VECTOR ( 'NONE', #10498, 1000.000000000000000 ) ;
#4417=FACE_OUTER_BOUND ( 'NONE', #4540, .T. ) ;
#4433=DIRECTION ( 'NONE',  ( -1.000000000000000000, 0.000000000000000000, 0.000000000000000000 ) ) ;
#4438=VERTEX_POINT ( 'NONE', #5089 ) ;
#4442=DIRECTION ( 'NONE',  ( 0.000000000000000000, 6.123233995736769734E-17, -1.000000000000000000 ) ) ;
#4450=LINE ( 'NONE', #2800, #1409 ) ;
#4451=DIRECTION ( 'NONE',  ( 1.899065700016719806E-16, 1.000000000000000000, 0.000000000000000000 ) ) ;
#4462=ORIENTED_EDGE ( 'NONE', *, *, #12422, .F. ) ;
#4472=EDGE_LOOP ( 'NONE', ( #6604, #12984, #6336, #4690 ) ) ;
#4473=LINE ( 'NONE', #1711, #15468 ) ;
#4477=DIRECTION ( 'NONE',  ( 1.000000000000000000, 0.000000000000000000, 0.000000000000000000 ) ) ;
#4499=ORIENTED_EDGE ( 'NONE', *, *, #7928, .F. ) ;
#4503=EDGE_CURVE ( 'NONE', #8531, #13096, #17843, .T. ) ;
#4515=DIRECTION ( 'NONE',  ( -1.000000000000000000, -4.037174635000570090E-16, 0.000000000000000000 ) ) ;
#4517=CARTESIAN_POINT ( 'NONE',  ( 0.9000000000000000222, 6.450000000000000178, 3.600000000000000089 ) ) ;
#4520=ADVANCED_FACE ( 'NONE', ( #12036 ), #736, .F. ) ;
#4521=( LENGTH_UNIT ( ) NAMED_UNIT ( * ) SI_UNIT ( .MILLI., .METRE. ) );
#4522=EDGE_LOOP ( 'NONE', ( #18097, #7771, #2406, #3522 ) ) ;
#4530=LINE ( 'NONE', #12976, #10314 ) ;
#4534=LINE ( 'NONE', #16210, #3523 ) ;
#4535=VERTEX_POINT ( 'NONE', #9540 ) ;
#4540=EDGE_LOOP ( 'NONE', ( #730, #18179, #4217, #8676 ) ) ;
#4545=VERTEX_POINT ( 'NONE', #12138 ) ;
#4552=EDGE_LOOP ( 'NONE', ( #15513, #5009, #992, #17069, #3967, #15017 ) ) ;
#4569=ORIENTED_EDGE ( 'NONE', *, *, #11877, .F. ) ;
#4575=PLANE ( 'NONE',  #11259 ) ;
#4591=PLANE ( 'NONE',  #17328 ) ;
#4593=ADVANCED_FACE ( 'NONE', ( #8152 ), #4239, .T. ) ;
#4595=EDGE_CURVE ( 'NONE', #11049, #8102, #5378, .T. ) ;
#4607=CARTESIAN_POINT ( 'NONE',  ( -1.399999999999999911, 0.5999999999999999778, 3.299999999999999822 ) ) ;
#4608=FACE_OUTER_BOUND ( 'NONE', #4283, .T. ) ;
#4619=CARTESIAN_POINT ( 'NONE',  ( -1.250000000000000000, 0.5999999999999999778, 6.100000000000000533 ) ) ;
#4620=LINE ( 'NONE', #10279, #7963 ) ;
#4625=VECTOR ( 'NONE', #3568, 1000.000000000000000 ) ;
#4627=VERTEX_POINT ( 'NONE', #11200 ) ;
#4631=ORIENTED_EDGE ( 'NONE', *, *, #2467, .T. ) ;
#4646=VECTOR ( 'NONE', #9136, 1000.000000000000000 ) ;
#4648=DIRECTION ( 'NONE',  ( -1.000000000000000000, 0.000000000000000000, 0.000000000000000000 ) ) ;
#4657=LINE ( 'NONE', #10313, #9099 ) ;
#4659=VERTEX_POINT ( 'NONE', #6760 ) ;
#4660=CARTESIAN_POINT ( 'NONE',  ( 1.399999999999999911, -7.000000000000000000, 3.299999999999999822 ) ) ;
#4665=VECTOR ( 'NONE', #14540, 1000.000000000000000 ) ;
#4678=DIRECTION ( 'NONE',  ( 0.000000000000000000, 6.123233995736769734E-17, -1.000000000000000000 ) ) ;
#4690=ORIENTED_EDGE ( 'NONE', *, *, #1266, .T. ) ;
#4698=VECTOR ( 'NONE', #7077, 1000.000000000000000 ) ;
#4707=CARTESIAN_POINT ( 'NONE',  ( 1.399999999999999911, 0.5999999999999999778, 6.100000000000000533 ) ) ;
#4712=ADVANCED_FACE ( 'NONE', ( #1377 ), #5735, .F. ) ;
#4723=ADVANCED_FACE ( 'NONE', ( #15386 ), #4329, .T. ) ;
#4736=VECTOR ( 'NONE', #9307, 1000.000000000000000 ) ;
#4737=CARTESIAN_POINT ( 'NONE',  ( 0.4000000000000000222, -1.399999999999999911, 5.100000000000000533 ) ) ;
#4739=EDGE_CURVE ( 'NONE', #13665, #5243, #2778, .T. ) ;
#4745=VERTEX_POINT ( 'NONE', #5648 ) ;
#4758=PLANE ( 'NONE',  #17638 ) ;
#4762=CARTESIAN_POINT ( 'NONE',  ( 1.000000000000000000, -6.000000000000000000, 3.299999999999999822 ) ) ;
#4770=EDGE_CURVE ( 'NONE', #10029, #2905, #91, .T. ) ;
#4773=( NAMED_UNIT ( * ) PLANE_ANGLE_UNIT ( ) SI_UNIT ( $, .RADIAN. ) );
#4775=ORIENTED_EDGE ( 'NONE', *, *, #14135, .T. ) ;
#4781=VECTOR ( 'NONE', #9207, 1000.000000000000000 ) ;
#4806=CARTESIAN_POINT ( 'NONE',  ( 0.5500000000000000444, 7.799999999999999822, 3.600000000000000089 ) ) ;
#4812=FACE_OUTER_BOUND ( 'NONE', #3282, .T. ) ;
#4821=CARTESIAN_POINT ( 'NONE',  ( -1.399999999999999911, -6.000000000000000000, 3.299999999999999822 ) ) ;
#4843=EDGE_CURVE ( 'NONE', #15809, #4957, #11899, .T. ) ;
#4849=CARTESIAN_POINT ( 'NONE',  ( 1.399999999999999911, -9.500000000000000000, 6.100000000000000533 ) ) ;
#4852=CARTESIAN_POINT ( 'NONE',  ( 1.000000000000000000, -7.000000000000000000, 5.700000000000000178 ) ) ;
#4857=CARTESIAN_POINT ( 'NONE',  ( -1.250000000000000000, 0.5999999999999999778, 7.599999999999999645 ) ) ;
#4859=ORIENTED_EDGE ( 'NONE', *, *, #16310, .T. ) ;
#4860=ORIENTED_EDGE ( 'NONE', *, *, #11178, .F. ) ;
#4863=CARTESIAN_POINT ( 'NONE',  ( 1.000000000000000000, -7.000000000000000000, 3.700000000000000178 ) ) ;
#4868=CARTESIAN_POINT ( 'NONE',  ( 1.800000000000000044, 7.799999999999999822, 1.600000000000000089 ) ) ;
#4872=EDGE_CURVE ( 'NONE', #8624, #8561, #17518, .T. ) ;
#4884=DIRECTION ( 'NONE',  ( 0.000000000000000000, 0.000000000000000000, -1.000000000000000000 ) ) ;
#4904=DIRECTION ( 'NONE',  ( -1.000000000000000000, 0.000000000000000000, 0.000000000000000000 ) ) ;
#4920=ORIENTED_EDGE ( 'NONE', *, *, #4739, .F. ) ;
#4938=VECTOR ( 'NONE', #152, 1000.000000000000000 ) ;
#4957=VERTEX_POINT ( 'NONE', #1063 ) ;
#4976=CARTESIAN_POINT ( 'NONE',  ( -1.250000000000000000, 5.012741699796949391, 5.100000000000000533 ) ) ;
#4981=VECTOR ( 'NONE', #16955, 1000.000000000000000 ) ;
#4984=ORIENTED_EDGE ( 'NONE', *, *, #10980, .T. ) ;
#4992=( GEOMETRIC_REPRESENTATION_CONTEXT ( 3 ) GLOBAL_UNCERTAINTY_ASSIGNED_CONTEXT ( ( #3983 ) ) GLOBAL_UNIT_ASSIGNED_CONTEXT ( ( #14596, #4773, #10424 ) ) REPRESENTATION_CONTEXT ( 'NONE', 'WORKASPACE' ) );
#4997=DIRECTION ( 'NONE',  ( 1.000000000000000000, 0.000000000000000000, 0.000000000000000000 ) ) ;
#5009=ORIENTED_EDGE ( 'NONE', *, *, #15246, .F. ) ;
#5011=ORIENTED_EDGE ( 'NONE', *, *, #3465, .F. ) ;
#5024=ORIENTED_EDGE ( 'NONE', *, *, #2120, .T. ) ;
#5025=DIRECTION ( 'NONE',  ( 0.000000000000000000, 0.000000000000000000, 1.000000000000000000 ) ) ;
#5026=DIRECTION ( 'NONE',  ( 0.000000000000000000, 0.000000000000000000, 1.000000000000000000 ) ) ;
#5031=VERTEX_POINT ( 'NONE', #12454 ) ;
#5041=ORIENTED_EDGE ( 'NONE', *, *, #12544, .F. ) ;
#5056=LINE ( 'NONE', #989, #16585 ) ;
#5057=CARTESIAN_POINT ( 'NONE',  ( -9.552245033349350628E-16, 7.799999999999999822, 4.776122516674680244E-16 ) ) ;
#5058=DIRECTION ( 'NONE',  ( 1.000000000000000000, 0.000000000000000000, 0.000000000000000000 ) ) ;
#5074=EDGE_CURVE ( 'NONE', #16255, #5452, #16531, .T. ) ;
#5077=CARTESIAN_POINT ( 'NONE',  ( -0.5500000000000000444, 6.450000000000000178, 3.600000000000000089 ) ) ;
#5083=DIRECTION ( 'NONE',  ( 1.000000000000000000, 0.000000000000000000, 0.000000000000000000 ) ) ;
#5087=CARTESIAN_POINT ( 'NONE',  ( -0.5500000000000000444, 7.799999999999999822, 1.600000000000000089 ) ) ;
#5089=CARTESIAN_POINT ( 'NONE',  ( 0.5000000000000000000, 5.762741699796949391, 6.100000000000000533 ) ) ;
#5101=ORIENTED_EDGE ( 'NONE', *, *, #4739, .T. ) ;
#5105=CARTESIAN_POINT ( 'NONE',  ( 1.399999999999999911, -8.000000000000000000, 3.299999999999999822 ) ) ;
#5108=EDGE_CURVE ( 'NONE', #4535, #6313, #10976, .T. ) ;
#5116=( BOUNDED_CURVE ( )  B_SPLINE_CURVE ( 3, ( #10259, #14613, #16022, #9044 ),
 .UNSPECIFIED., .F., .F. ) 
 B_SPLINE_CURVE_WITH_KNOTS ( ( 4, 4 ),
 ( 0.000000000000000000, 1.000000000000000000 ),
 .UNSPECIFIED. ) 
 CURVE ( )  GEOMETRIC_REPRESENTATION_ITEM ( )  RATIONAL_B_SPLINE_CURVE ( ( 1.000000000000000000, 0.8047378541243649375, 0.8047378541243649375, 1.000000000000000000 ) ) 
 REPRESENTATION_ITEM ( '' )  );
#5117=VERTEX_POINT ( 'NONE', #6807 ) ;
#5120=ORIENTED_EDGE ( 'NONE', *, *, #582, .T. ) ;
#5147=CARTESIAN_POINT ( 'NONE',  ( 1.399999999999999911, 0.5999999999999999778, 3.299999999999999822 ) ) ;
#5155=DIRECTION ( 'NONE',  ( 1.000000000000000000, 8.074349270001130318E-16, 0.000000000000000000 ) ) ;
#5156=EDGE_CURVE ( 'NONE', #18019, #490, #13933, .T. ) ;
#5159=CARTESIAN_POINT ( 'NONE',  ( 1.000000000000000000, -5.500000000000000000, 5.100000000000000533 ) ) ;
#5164=CARTESIAN_POINT ( 'NONE',  ( 1.399999999999999911, -7.000000000000000000, 6.100000000000000533 ) ) ;
#5181=CARTESIAN_POINT ( 'NONE',  ( 0.9000000000000000222, 6.450000000000000178, 3.600000000000000089 ) ) ;
#5182=EDGE_CURVE ( 'NONE', #16755, #18019, #8423, .T. ) ;
#5183=DIRECTION ( 'NONE',  ( -1.233581138472399909E-16, 1.000000000000000000, 0.000000000000000000 ) ) ;
#5194=ORIENTED_EDGE ( 'NONE', *, *, #9614, .F. ) ;
#5195=VERTEX_POINT ( 'NONE', #14298 ) ;
#5199=DIRECTION ( 'NONE',  ( 7.930164461608259947E-17, 0.000000000000000000, 1.000000000000000000 ) ) ;
#5202=ORIENTED_EDGE ( 'NONE', *, *, #16644, .T. ) ;
#5219=FACE_OUTER_BOUND ( 'NONE', #13671, .T. ) ;
#5222=DIRECTION ( 'NONE',  ( 1.899065700016719806E-16, 1.000000000000000000, 0.000000000000000000 ) ) ;
#5226=CARTESIAN_POINT ( 'NONE',  ( 1.000000000000000000, -6.000000000000000000, 5.100000000000000533 ) ) ;
#5243=VERTEX_POINT ( 'NONE', #18257 ) ;
#5258=VECTOR ( 'NONE', #17401, 1000.000000000000000 ) ;
#5259=FACE_OUTER_BOUND ( 'NONE', #3499, .T. ) ;
#5262=VERTEX_POINT ( 'NONE', #11518 ) ;
#5272=DIRECTION ( 'NONE',  ( 0.000000000000000000, -1.000000000000000000, 8.673617379884027583E-16 ) ) ;
#5273=EDGE_LOOP ( 'NONE', ( #2821, #10735, #18043, #8829, #13549, #17565, #2677, #2846, #7741, #4236, #16037, #11143, #16726, #18151, #3342, #12368 ) ) ;
#5283=DIRECTION ( 'NONE',  ( 0.000000000000000000, 1.000000000000000000, 0.000000000000000000 ) ) ;
#5290=CARTESIAN_POINT ( 'NONE',  ( 7.233457020361919865E-16, 4.000000000000000000, 5.100000000000000533 ) ) ;
#5294=CARTESIAN_POINT ( 'NONE',  ( 1.250000000000000000, 7.799999999999999822, 6.100000000000000533 ) ) ;
#5300=VERTEX_POINT ( 'NONE', #7093 ) ;
#5301=DIRECTION ( 'NONE',  ( 1.000000000000000000, 1.746418240983389920E-16, 1.110223024625159992E-16 ) ) ;
#5305=PLANE ( 'NONE',  #15882 ) ;
#5314=VECTOR ( 'NONE', #15118, 1000.000000000000000 ) ;
#5318=EDGE_LOOP ( 'NONE', ( #4859, #14469, #3158, #1165 ) ) ;
#5319=ADVANCED_FACE ( 'NONE', ( #584, #10203 ), #6306, .F. ) ;
#5344=ORIENTED_EDGE ( 'NONE', *, *, #10953, .T. ) ;
#5347=CARTESIAN_POINT ( 'NONE',  ( -1.000000000000000000, -5.000000000000000000, 3.299999999999999822 ) ) ;
#5359=EDGE_CURVE ( 'NONE', #7455, #7321, #7616, .T. ) ;
#5371=VECTOR ( 'NONE', #2793, 1000.000000000000000 ) ;
#5373=EDGE_CURVE ( 'NONE', #7510, #5452, #8994, .T. ) ;
#5378=LINE ( 'NONE', #2593, #12491 ) ;
#5394=DIRECTION ( 'NONE',  ( -3.392348130799090196E-16, 1.000000000000000000, 1.233581138472399909E-16 ) ) ;
#5414=EDGE_CURVE ( 'NONE', #13613, #12574, #13045, .T. ) ;
#5422=LINE ( 'NONE', #12736, #12348 ) ;
#5428=CARTESIAN_POINT ( 'NONE',  ( -0.5500000000000000444, 2.050000000000000266, 3.600000000000000089 ) ) ;
#5448=DIRECTION ( 'NONE',  ( 0.000000000000000000, 0.000000000000000000, 1.000000000000000000 ) ) ;
#5449=CARTESIAN_POINT ( 'NONE',  ( -1.399999999999999911, -6.000000000000000000, 5.100000000000000533 ) ) ;
#5452=VERTEX_POINT ( 'NONE', #17585 ) ;
#5458=EDGE_CURVE ( 'NONE', #14617, #12922, #11887, .T. ) ;
#5472=ORIENTED_EDGE ( 'NONE', *, *, #4872, .T. ) ;
#5475=FACE_OUTER_BOUND ( 'NONE', #729, .T. ) ;
#5478=CARTESIAN_POINT ( 'NONE',  ( -1.399999999999999911, -5.500000000000000000, 6.100000000000000533 ) ) ;
#5498=ORIENTED_EDGE ( 'NONE', *, *, #4503, .F. ) ;
#5499=CARTESIAN_POINT ( 'NONE',  ( -0.9000000000000000222, -10.00000000000000000, 3.799999999999999822 ) ) ;
#5505=ORIENTED_EDGE ( 'NONE', *, *, #10953, .F. ) ;
#5507=DIRECTION ( 'NONE',  ( 1.224646799147350002E-16, -1.000000000000000000, -6.123233995736769734E-17 ) ) ;
#5516=ADVANCED_FACE ( 'NONE', ( #6789 ), #12437, .T. ) ;
#5530=DIRECTION ( 'NONE',  ( 0.000000000000000000, 0.000000000000000000, 1.000000000000000000 ) ) ;
#5531=ORIENTED_EDGE ( 'NONE', *, *, #9721, .T. ) ;
#5542=AXIS2_PLACEMENT_3D ( 'NONE', #4061, #9903, #12687 ) ;
#5543=AXIS2_PLACEMENT_3D ( 'NONE', #10739, #10831, #16386 ) ;
#5548=AXIS2_PLACEMENT_3D ( 'NONE', #1392, #6276, #4884 ) ;
#5564=LINE ( 'NONE', #12868, #2365 ) ;
#5565=ORIENTED_EDGE ( 'NONE', *, *, #7447, .T. ) ;
#5572=CARTESIAN_POINT ( 'NONE',  ( 0.5500000000000000444, -2.399999999999999911, 3.299999999999999822 ) ) ;
#5578=VECTOR ( 'NONE', #15644, 1000.000000000000000 ) ;
#5580=CARTESIAN_POINT ( 'NONE',  ( 1.800000000000000044, 0.5999999999999999778, 7.599999999999999645 ) ) ;
#5593=VECTOR ( 'NONE', #15093, 1000.000000000000000 ) ;
#5607=CARTESIAN_POINT ( 'NONE',  ( 1.399999999999999911, -9.500000000000000000, 3.299999999999999822 ) ) ;
#5611=CARTESIAN_POINT ( 'NONE',  ( 7.347880794884119736E-16, -6.000000000000000000, -3.673940397442060361E-16 ) ) ;
#5641=CARTESIAN_POINT ( 'NONE',  ( -1.800000000000000044, 0.5999999999999999778, 7.599999999999999645 ) ) ;
#5643=VECTOR ( 'NONE', #10989, 1000.000000000000000 ) ;
#5648=CARTESIAN_POINT ( 'NONE',  ( 7.233457020361919865E-16, 4.000000000000000000, 5.100000000000000533 ) ) ;
#5659=ORIENTED_EDGE ( 'NONE', *, *, #6875, .F. ) ;
#5666=CARTESIAN_POINT ( 'NONE',  ( -0.4000000000000000222, -1.399999999999999911, 6.100000000000000533 ) ) ;
#5673=LINE ( 'NONE', #5580, #6670 ) ;
#5674=ADVANCED_FACE ( 'NONE', ( #14196 ), #11580, .T. ) ;
#5694=ORIENTED_EDGE ( 'NONE', *, *, #14236, .F. ) ;
#5702=ORIENTED_EDGE ( 'NONE', *, *, #10980, .F. ) ;
#5709=DIRECTION ( 'NONE',  ( -1.644774851296529842E-16, 1.000000000000000000, 0.000000000000000000 ) ) ;
#5726=ORIENTED_EDGE ( 'NONE', *, *, #10487, .T. ) ;
#5730=ORIENTED_EDGE ( 'NONE', *, *, #13350, .F. ) ;
#5735=PLANE ( 'NONE',  #9221 ) ;
#5744=DIRECTION ( 'NONE',  ( 4.440892098500630106E-16, -1.000000000000000000, 0.000000000000000000 ) ) ;
#5761=DIRECTION ( 'NONE',  ( 1.000000000000000000, 0.000000000000000000, 0.000000000000000000 ) ) ;
#5767=CARTESIAN_POINT ( 'NONE',  ( -1.399999999999999911, -6.000000000000000000, 3.299999999999999822 ) ) ;
#5779=ORIENTED_EDGE ( 'NONE', *, *, #17063, .T. ) ;
#5787=PLANE ( 'NONE',  #7938 ) ;
#5789=ORIENTED_EDGE ( 'NONE', *, *, #7553, .T. ) ;
#5790=DIRECTION ( 'NONE',  ( 2.379049338482479710E-16, 0.000000000000000000, 1.000000000000000000 ) ) ;
#5800=CARTESIAN_POINT ( 'NONE',  ( 0.5500000000000000444, 0.5999999999999999778, 3.299999999999999822 ) ) ;
#5806=CARTESIAN_POINT ( 'NONE',  ( -1.250000000000000000, 3.881370849898470254, 5.100000000000000533 ) ) ;
#5809=ORIENTED_EDGE ( 'NONE', *, *, #3144, .T. ) ;
#5818=DIRECTION ( 'NONE',  ( -3.289549702593060178E-16, 1.000000000000000000, 0.000000000000000000 ) ) ;
#5820=VECTOR ( 'NONE', #15634, 1000.000000000000000 ) ;
#5823=CARTESIAN_POINT ( 'NONE',  ( 0.000000000000000000, 0.000000000000000000, 5.100000000000000533 ) ) ;
#5830=VERTEX_POINT ( 'NONE', #740 ) ;
#5850=VECTOR ( 'NONE', #5960, 1000.000000000000000 ) ;
#5856=DIRECTION ( 'NONE',  ( 1.000000000000000000, 0.000000000000000000, 0.000000000000000000 ) ) ;
#5875=DIRECTION ( 'NONE',  ( 2.220446049250309876E-16, -1.000000000000000000, 0.000000000000000000 ) ) ;
#5877=ORIENTED_EDGE ( 'NONE', *, *, #14281, .F. ) ;
#5883=ORIENTED_EDGE ( 'NONE', *, *, #10606, .T. ) ;
#5888=VERTEX_POINT ( 'NONE', #2136 ) ;
#5895=EDGE_CURVE ( 'NONE', #13769, #8163, #14626, .T. ) ;
#5897=FACE_BOUND ( 'NONE', #4279, .T. ) ;
#5922=PLANE ( 'NONE',  #256 ) ;
#5942=EDGE_CURVE ( 'NONE', #13228, #6816, #3412, .T. ) ;
#5943=CARTESIAN_POINT ( 'NONE',  ( -0.9000000000000000222, 6.450000000000000178, 3.600000000000000089 ) ) ;
#5949=PLANE ( 'NONE',  #847 ) ;
#5958=ORIENTED_EDGE ( 'NONE', *, *, #2102, .F. ) ;
#5960=DIRECTION ( 'NONE',  ( 0.000000000000000000, 0.000000000000000000, 1.000000000000000000 ) ) ;
#5963=DIRECTION ( 'NONE',  ( -1.000000000000000000, 0.000000000000000000, 0.000000000000000000 ) ) ;
#5964=DIRECTION ( 'NONE',  ( 0.000000000000000000, -1.000000000000000000, 0.000000000000000000 ) ) ;
#5966=ORIENTED_EDGE ( 'NONE', *, *, #13240, .F. ) ;
#5974=EDGE_CURVE ( 'NONE', #3213, #11589, #6666, .T. ) ;
#5995=ADVANCED_FACE ( 'NONE', ( #10939 ), #10837, .F. ) ;
#5999=CARTESIAN_POINT ( 'NONE',  ( 1.250000000000000000, 0.5999999999999999778, 6.100000000000000533 ) ) ;
#6015=ORIENTED_EDGE ( 'NONE', *, *, #2087, .F. ) ;
#6041=CARTESIAN_POINT ( 'NONE',  ( 8.549934884138839976E-16, 6.262741699796950279, 5.100000000000000533 ) ) ;
#6046=AXIS2_PLACEMENT_3D ( 'NONE', #13780, #2580, #5272 ) ;
#6063=ORIENTED_EDGE ( 'NONE', *, *, #1894, .F. ) ;
#6067=DIRECTION ( 'NONE',  ( 1.224646799147350002E-16, -1.000000000000000000, -6.123233995736769734E-17 ) ) ;
#6075=ORIENTED_EDGE ( 'NONE', *, *, #14817, .F. ) ;
#6079=DIRECTION ( 'NONE',  ( 1.000000000000000000, 0.000000000000000000, -1.110223024625159992E-16 ) ) ;
#6096=ORIENTED_EDGE ( 'NONE', *, *, #13431, .T. ) ;
#6099=ORIENTED_EDGE ( 'NONE', *, *, #18216, .T. ) ;
#6119=VERTEX_POINT ( 'NONE', #4517 ) ;
#6124=AXIS2_PLACEMENT_3D ( 'NONE', #8655, #8840, #328 ) ;
#6188=CARTESIAN_POINT ( 'NONE',  ( 1.250000000000000000, 7.799999999999999822, 7.599999999999999645 ) ) ;
#6189=EDGE_LOOP ( 'NONE', ( #17408, #12240, #16123, #8207 ) ) ;
#6191=CARTESIAN_POINT ( 'NONE',  ( 7.069631497386979886E-16, 5.131370849898479136, 5.100000000000000533 ) ) ;
#6193=PLANE ( 'NONE',  #2274 ) ;
#6200=ADVANCED_FACE ( 'NONE', ( #283 ), #5922, .T. ) ;
#6204=CARTESIAN_POINT ( 'NONE',  ( 8.416823969807580597E-17, 6.262741699796950279, 5.100000000000000533 ) ) ;
#6210=VECTOR ( 'NONE', #5790, 1000.000000000000000 ) ;
#6221=DIRECTION ( 'NONE',  ( 0.000000000000000000, -1.000000000000000000, -8.881784197001250351E-16 ) ) ;
#6230=ORIENTED_EDGE ( 'NONE', *, *, #10610, .T. ) ;
#6233=CARTESIAN_POINT ( 'NONE',  ( 1.399999999999999911, -6.000000000000000000, 5.100000000000000533 ) ) ;
#6245=CARTESIAN_POINT ( 'NONE',  ( 0.5500000000000000444, 6.450000000000000178, 3.600000000000000089 ) ) ;
#6254=ORIENTED_EDGE ( 'NONE', *, *, #2230, .F. ) ;
#6265=EDGE_CURVE ( 'NONE', #12426, #16167, #368, .T. ) ;
#6276=DIRECTION ( 'NONE',  ( 0.000000000000000000, -1.000000000000000000, 0.000000000000000000 ) ) ;
#6288=DIRECTION ( 'NONE',  ( 1.189524669241239855E-16, -1.000000000000000000, 0.000000000000000000 ) ) ;
#6296=VERTEX_POINT ( 'NONE', #7761 ) ;
#6306=PLANE ( 'NONE',  #14123 ) ;
#6313=VERTEX_POINT ( 'NONE', #10749 ) ;
#6336=ORIENTED_EDGE ( 'NONE', *, *, #17482, .T. ) ;
#6339=CARTESIAN_POINT ( 'NONE',  ( -1.250000000000000000, 7.799999999999999822, 7.599999999999999645 ) ) ;
#6352=EDGE_LOOP ( 'NONE', ( #11305, #15885, #14830, #16309, #2217, #12421, #14481, #16002, #15049, #272, #10586, #8373, #15420, #5565 ) ) ;
#6362=ORIENTED_EDGE ( 'NONE', *, *, #15735, .F. ) ;
#6363=LINE ( 'NONE', #2021, #1386 ) ;
#6364=DIRECTION ( 'NONE',  ( -0.000000000000000000, 1.000000000000000000, 0.000000000000000000 ) ) ;
#6379=DIRECTION ( 'NONE',  ( -2.018587317500279868E-16, 1.000000000000000000, 5.046468293750709530E-17 ) ) ;
#6389=EDGE_LOOP ( 'NONE', ( #15372, #2142, #8196, #1003 ) ) ;
#6394=AXIS2_PLACEMENT_3D ( 'NONE', #12196, #6440, #5058 ) ;
#6397=CARTESIAN_POINT ( 'NONE',  ( 0.5500000000000000444, -2.399999999999999911, 3.600000000000000089 ) ) ;
#6402=FACE_OUTER_BOUND ( 'NONE', #15158, .T. ) ;
#6405=VECTOR ( 'NONE', #2623, 1000.000000000000000 ) ;
#6419=PLANE ( 'NONE',  #15009 ) ;
#6424=AXIS2_PLACEMENT_3D ( 'NONE', #15739, #12948, #12858 ) ;
#6434=AXIS2_PLACEMENT_3D ( 'NONE', #16630, #5507, #15343 ) ;
#6439=DIRECTION ( 'NONE',  ( 0.000000000000000000, 0.000000000000000000, 1.000000000000000000 ) ) ;
#6440=DIRECTION ( 'NONE',  ( 0.000000000000000000, 0.000000000000000000, 1.000000000000000000 ) ) ;
#6456=VERTEX_POINT ( 'NONE', #5641 ) ;
#6464=CARTESIAN_POINT ( 'NONE',  ( 0.9000000000000000222, 2.050000000000000266, 3.600000000000000089 ) ) ;
#6469=ORIENTED_EDGE ( 'NONE', *, *, #129, .F. ) ;
#6472=VERTEX_POINT ( 'NONE', #17009 ) ;
#6481=LINE ( 'NONE', #12140, #770 ) ;
#6484=LINE ( 'NONE', #5290, #5314 ) ;
#6490=VECTOR ( 'NONE', #17213, 1000.000000000000000 ) ;
#6491=VERTEX_POINT ( 'NONE', #7135 ) ;
#6518=CARTESIAN_POINT ( 'NONE',  ( -0.5500000000000000444, 7.799999999999999822, 1.600000000000000089 ) ) ;
#6526=CARTESIAN_POINT ( 'NONE',  ( 0.5000000000000000000, 4.631370849898480024, 5.100000000000000533 ) ) ;
#6537=EDGE_CURVE ( 'NONE', #2694, #8350, #12770, .T. ) ;
#6542=LINE ( 'NONE', #12108, #208 ) ;
#6543=EDGE_CURVE ( 'NONE', #10849, #10826, #11375, .T. ) ;
#6544=ORIENTED_EDGE ( 'NONE', *, *, #9976, .F. ) ;
#6555=ORIENTED_EDGE ( 'NONE', *, *, #13500, .F. ) ;
#6577=CARTESIAN_POINT ( 'NONE',  ( -0.5500000000000000444, 2.050000000000000266, 3.600000000000000089 ) ) ;
#6581=CARTESIAN_POINT ( 'NONE',  ( 1.250000000000000000, 3.500000000000000000, 5.100000000000000533 ) ) ;
#6592=CARTESIAN_POINT ( 'NONE',  ( -1.000000000000000000, -5.000000000000000000, 6.100000000000000533 ) ) ;
#6604=ORIENTED_EDGE ( 'NONE', *, *, #15171, .F. ) ;
#6605=CARTESIAN_POINT ( 'NONE',  ( 1.399999999999999911, 0.5999999999999999778, 6.100000000000000533 ) ) ;
#6608=DIRECTION ( 'NONE',  ( 2.379049338482479710E-16, 0.000000000000000000, 1.000000000000000000 ) ) ;
#6621=LINE ( 'NONE', #11909, #18026 ) ;
#6629=ORIENTED_EDGE ( 'NONE', *, *, #4770, .F. ) ;
#6634=LINE ( 'NONE', #14986, #8802 ) ;
#6636=EDGE_CURVE ( 'NONE', #9952, #3716, #9027, .T. ) ;
#6638=LINE ( 'NONE', #5159, #5593 ) ;
#6641=EDGE_CURVE ( 'NONE', #6119, #4535, #13127, .T. ) ;
#6649=ORIENTED_EDGE ( 'NONE', *, *, #8364, .F. ) ;
#6651=ORIENTED_EDGE ( 'NONE', *, *, #3722, .F. ) ;
#6660=ADVANCED_FACE ( 'NONE', ( #10237 ), #15909, .T. ) ;
#6666=LINE ( 'NONE', #17849, #11481 ) ;
#6670=VECTOR ( 'NONE', #5394, 1000.000000000000000 ) ;
#6671=LINE ( 'NONE', #13432, #15199 ) ;
#6679=CARTESIAN_POINT ( 'NONE',  ( 0.5500000000000000444, 0.5999999999999999778, 1.600000000000000089 ) ) ;
#6680=DIRECTION ( 'NONE',  ( -2.220446049250309876E-16, 0.000000000000000000, 1.000000000000000000 ) ) ;
#6681=VECTOR ( 'NONE', #1329, 1000.000000000000000 ) ;
#6706=CARTESIAN_POINT ( 'NONE',  ( -1.800000000000000044, 7.799999999999999822, 7.599999999999999645 ) ) ;
#6714=VECTOR ( 'NONE', #275, 1000.000000000000000 ) ;
#6715=DIRECTION ( 'NONE',  ( 0.000000000000000000, 6.123233995736769734E-17, -1.000000000000000000 ) ) ;
#6740=EDGE_CURVE ( 'NONE', #10826, #14727, #619, .T. ) ;
#6741=VECTOR ( 'NONE', #2092, 1000.000000000000000 ) ;
#6748=ORIENTED_EDGE ( 'NONE', *, *, #2958, .F. ) ;
#6755=EDGE_CURVE ( 'NONE', #10460, #14390, #10616, .T. ) ;
#6760=CARTESIAN_POINT ( 'NONE',  ( -1.250000000000000000, 3.500000000000000000, 6.100000000000000533 ) ) ;
#6775=PRODUCT_DEFINITION_CONTEXT ( 'detailed design', #17577, 'design' ) ;
#6777=ORIENTED_EDGE ( 'NONE', *, *, #6755, .T. ) ;
#6779=EDGE_CURVE ( 'NONE', #16856, #356, #6542, .T. ) ;
#6784=PLANE ( 'NONE',  #7887 ) ;
#6789=FACE_OUTER_BOUND ( 'NONE', #12000, .T. ) ;
#6801=VERTEX_POINT ( 'NONE', #798 ) ;
#6807=CARTESIAN_POINT ( 'NONE',  ( -1.399999999999999911, -7.000000000000000000, 6.100000000000000533 ) ) ;
#6811=ADVANCED_FACE ( 'NONE', ( #18003 ), #2478, .T. ) ;
#6813=DIRECTION ( 'NONE',  ( -0.7071067811865470176, -0.7071067811865480168, 0.000000000000000000 ) ) ;
#6816=VERTEX_POINT ( 'NONE', #5347 ) ;
#6818=PLANE ( 'NONE',  #2585 ) ;
#6830=DIRECTION ( 'NONE',  ( -1.000000000000000000, -1.110223024625159992E-16, 1.110223024625159992E-16 ) ) ;
#6844=ORIENTED_EDGE ( 'NONE', *, *, #11653, .T. ) ;
#6847=CARTESIAN_POINT ( 'NONE',  ( 6.429395695523600208E-16, 3.500000000000000000, 5.100000000000000533 ) ) ;
#6852=DIRECTION ( 'NONE',  ( 0.000000000000000000, -1.000000000000000000, -6.167905692361979821E-17 ) ) ;
#6859=CARTESIAN_POINT ( 'NONE',  ( 1.399999999999999911, -6.000000000000000000, 3.299999999999999822 ) ) ;
#6875=EDGE_CURVE ( 'NONE', #2335, #7455, #7942, .T. ) ;
#6878=EDGE_CURVE ( 'NONE', #10219, #16165, #1177, .T. ) ;
#6887=ORIENTED_EDGE ( 'NONE', *, *, #6537, .F. ) ;
#6889=VECTOR ( 'NONE', #5448, 1000.000000000000000 ) ;
#6897=ADVANCED_FACE ( 'NONE', ( #12285 ), #16550, .T. ) ;
#6899=DIRECTION ( 'NONE',  ( -0.7071067811865470176, -0.7071067811865480168, 0.000000000000000000 ) ) ;
#6907=ORIENTED_EDGE ( 'NONE', *, *, #16883, .F. ) ;
#6915=DIRECTION ( 'NONE',  ( 0.000000000000000000, -4.482164234210289821E-32, -1.000000000000000000 ) ) ;
#6920=CARTESIAN_POINT ( 'NONE',  ( 1.800000000000000044, 0.5999999999999999778, 7.599999999999999645 ) ) ;
#6923=LINE ( 'NONE', #13960, #12506 ) ;
#6924=LINE ( 'NONE', #16831, #8290 ) ;
#6927=VERTEX_POINT ( 'NONE', #1631 ) ;
#6943=LINE ( 'NONE', #8620, #12423 ) ;
#6954=DIRECTION ( 'NONE',  ( 1.233581138472399909E-16, 6.167905692361979821E-17, -1.000000000000000000 ) ) ;
#6956=VECTOR ( 'NONE', #10692, 1000.000000000000000 ) ;
#6958=LINE ( 'NONE', #18049, #14091 ) ;
#6959=DIRECTION ( 'NONE',  ( 1.110223024625159992E-16, 0.000000000000000000, -1.000000000000000000 ) ) ;
#6969=ORIENTED_EDGE ( 'NONE', *, *, #5895, .T. ) ;
#7010=VECTOR ( 'NONE', #1184, 1000.000000000000000 ) ;
#7016=ORIENTED_EDGE ( 'NONE', *, *, #9721, .F. ) ;
#7039=DIRECTION ( 'NONE',  ( 1.110223024625159992E-16, 2.220446049250309876E-16, -1.000000000000000000 ) ) ;
#7041=DIRECTION ( 'NONE',  ( 0.000000000000000000, -1.000000000000000000, 0.000000000000000000 ) ) ;
#7055=ORIENTED_EDGE ( 'NONE', *, *, #6875, .T. ) ;
#7066=CARTESIAN_POINT ( 'NONE',  ( 1.800000000000000044, 0.5999999999999999778, 1.600000000000000089 ) ) ;
#7077=DIRECTION ( 'NONE',  ( 1.110223024625159992E-16, 0.000000000000000000, -1.000000000000000000 ) ) ;
#7093=CARTESIAN_POINT ( 'NONE',  ( -0.5500000000000000444, 6.450000000000000178, 3.600000000000000089 ) ) ;
#7097=CARTESIAN_POINT ( 'NONE',  ( -1.800000000000000044, 0.5999999999999999778, 7.599999999999999645 ) ) ;
#7113=LINE ( 'NONE', #17165, #12343 ) ;
#7135=CARTESIAN_POINT ( 'NONE',  ( 0.5500000000000000444, 7.799999999999999822, 1.600000000000000089 ) ) ;
#7153=CARTESIAN_POINT ( 'NONE',  ( 1.250000000000000000, 6.144112549695430303, 5.100000000000000533 ) ) ;
#7163=DIRECTION ( 'NONE',  ( 2.960594732333750117E-16, -1.000000000000000000, 0.000000000000000000 ) ) ;
#7181=LINE ( 'NONE', #7445, #15581 ) ;
#7205=CARTESIAN_POINT ( 'NONE',  ( 0.5000000000000000000, 5.762741699796949391, 5.100000000000000533 ) ) ;
#7217=CARTESIAN_POINT ( 'NONE',  ( -0.4000000000000000222, -1.399999999999999911, 5.100000000000000533 ) ) ;
#7222=DIRECTION ( 'NONE',  ( 1.000000000000000000, 0.000000000000000000, 0.000000000000000000 ) ) ;
#7224=DIRECTION ( 'NONE',  ( 1.586032892321649771E-16, -1.000000000000000000, 0.000000000000000000 ) ) ;
#7229=LINE ( 'NONE', #12871, #13421 ) ;
#7236=EDGE_CURVE ( 'NONE', #6119, #3213, #7113, .T. ) ;
#7242=LINE ( 'NONE', #9746, #11157 ) ;
#7243=DIRECTION ( 'NONE',  ( -3.965082230804129973E-17, 0.000000000000000000, -1.000000000000000000 ) ) ;
#7245=EDGE_CURVE ( 'NONE', #5452, #15809, #8583, .T. ) ;
#7249=LINE ( 'NONE', #5943, #4698 ) ;
#7250=ORIENTED_EDGE ( 'NONE', *, *, #11877, .T. ) ;
#7260=ORIENTED_EDGE ( 'NONE', *, *, #2272, .T. ) ;
#7264=DIRECTION ( 'NONE',  ( -1.000000000000000000, -2.018587317500279868E-16, -1.110223024625159992E-16 ) ) ;
#7270=ADVANCED_FACE ( 'NONE', ( #316 ), #10467, .F. ) ;
#7272=DIRECTION ( 'NONE',  ( -1.000000000000000000, 0.000000000000000000, 0.000000000000000000 ) ) ;
#7315=PLANE ( 'NONE',  #2192 ) ;
#7321=VERTEX_POINT ( 'NONE', #17415 ) ;
#7332=VECTOR ( 'NONE', #17734, 1000.000000000000000 ) ;
#7336=EDGE_CURVE ( 'NONE', #3539, #4745, #12995, .T. ) ;
#7339=DIRECTION ( 'NONE',  ( 0.000000000000000000, 0.000000000000000000, -1.000000000000000000 ) ) ;
#7346=ORIENTED_EDGE ( 'NONE', *, *, #16845, .F. ) ;
#7354=ORIENTED_EDGE ( 'NONE', *, *, #3866, .F. ) ;
#7358=VECTOR ( 'NONE', #3616, 1000.000000000000000 ) ;
#7367=VECTOR ( 'NONE', #7163, 1000.000000000000000 ) ;
#7394=LINE ( 'NONE', #438, #13320 ) ;
#7408=EDGE_LOOP ( 'NONE', ( #7354, #4163, #6063, #6777 ) ) ;
#7413=EDGE_CURVE ( 'NONE', #13613, #16121, #13084, .T. ) ;
#7423=LINE ( 'NONE', #115, #8841 ) ;
#7445=CARTESIAN_POINT ( 'NONE',  ( 1.399999999999999911, -5.500000000000000000, 6.100000000000000533 ) ) ;
#7446=DIRECTION ( 'NONE',  ( -2.220446049250319983E-16, 0.000000000000000000, -1.000000000000000000 ) ) ;
#7447=EDGE_CURVE ( 'NONE', #14738, #1479, #17499, .T. ) ;
#7455=VERTEX_POINT ( 'NONE', #16047 ) ;
#7484=LINE ( 'NONE', #17187, #8503 ) ;
#7488=CARTESIAN_POINT ( 'NONE',  ( 0.5500000000000000444, 2.050000000000000266, 1.600000000000000089 ) ) ;
#7508=DIRECTION ( 'NONE',  ( -1.000000000000000000, -1.189524669241239855E-16, -4.716563129111599823E-33 ) ) ;
#7510=VERTEX_POINT ( 'NONE', #16598 ) ;
#7516=DIRECTION ( 'NONE',  ( 0.000000000000000000, 0.000000000000000000, 1.000000000000000000 ) ) ;
#7526=VECTOR ( 'NONE', #17469, 1000.000000000000000 ) ;
#7530=LINE ( 'NONE', #14303, #10541 ) ;
#7553=EDGE_CURVE ( 'NONE', #8624, #2681, #8509, .T. ) ;
#7556=VERTEX_POINT ( 'NONE', #9833 ) ;
#7561=DIRECTION ( 'NONE',  ( 1.644774851296529842E-16, -1.000000000000000000, 0.000000000000000000 ) ) ;
#7562=ADVANCED_FACE ( 'NONE', ( #13910 ), #1504, .T. ) ;
#7576=EDGE_CURVE ( 'NONE', #7455, #5117, #12880, .T. ) ;
#7595=VECTOR ( 'NONE', #7561, 1000.000000000000000 ) ;
#7596=DIRECTION ( 'NONE',  ( -1.746418240983389920E-16, 1.000000000000000000, 0.000000000000000000 ) ) ;
#7601=ORIENTED_EDGE ( 'NONE', *, *, #2102, .T. ) ;
#7616=LINE ( 'NONE', #1804, #13529 ) ;
#7633=ORIENTED_EDGE ( 'NONE', *, *, #7669, .T. ) ;
#7637=VECTOR ( 'NONE', #16186, 1000.000000000000114 ) ;
#7646=ORIENTED_EDGE ( 'NONE', *, *, #5156, .T. ) ;
#7652=VERTEX_POINT ( 'NONE', #14074 ) ;
#7654=DIRECTION ( 'NONE',  ( -1.224646799147350002E-16, 1.000000000000000000, 6.123233995736769734E-17 ) ) ;
#7669=EDGE_CURVE ( 'NONE', #13769, #2785, #1224, .T. ) ;
#7677=LINE ( 'NONE', #7859, #7889 ) ;
#7678=CARTESIAN_POINT ( 'NONE',  ( -0.4000000000000000222, -1.399999999999999911, 5.100000000000000533 ) ) ;
#7697=ORIENTED_EDGE ( 'NONE', *, *, #12212, .F. ) ;
#7723=ORIENTED_EDGE ( 'NONE', *, *, #1236, .T. ) ;
#7726=DIRECTION ( 'NONE',  ( -1.000000000000000000, 7.105427357601000281E-16, -1.776356839400249824E-16 ) ) ;
#7732=ORIENTED_EDGE ( 'NONE', *, *, #2087, .T. ) ;
#7733=LINE ( 'NONE', #2378, #3470 ) ;
#7738=DIRECTION ( 'NONE',  ( 0.000000000000000000, -1.000000000000000000, 0.000000000000000000 ) ) ;
#7741=ORIENTED_EDGE ( 'NONE', *, *, #10610, .F. ) ;
#7761=CARTESIAN_POINT ( 'NONE',  ( 0.5000000000000000000, 5.762741699796949391, 5.100000000000000533 ) ) ;
#7762=FACE_OUTER_BOUND ( 'NONE', #16292, .T. ) ;
#7764=CARTESIAN_POINT ( 'NONE',  ( -1.250000000000000000, 3.881370849898470254, 6.100000000000000533 ) ) ;
#7771=ORIENTED_EDGE ( 'NONE', *, *, #12318, .F. ) ;
#7779=CARTESIAN_POINT ( 'NONE',  ( 1.800000000000000044, 0.5999999999999999778, 1.600000000000000089 ) ) ;
#7812=CARTESIAN_POINT ( 'NONE',  ( -0.4058874503045720172, 7.799999999999999822, 6.100000000000000533 ) ) ;
#7828=CARTESIAN_POINT ( 'NONE',  ( -0.5500000000000000444, 6.450000000000000178, 1.600000000000000089 ) ) ;
#7835=DIRECTION ( 'NONE',  ( 1.000000000000000000, 0.000000000000000000, 0.000000000000000000 ) ) ;
#7854=DIRECTION ( 'NONE',  ( 0.000000000000000000, 0.000000000000000000, 1.000000000000000000 ) ) ;
#7857=DIRECTION ( 'NONE',  ( 1.531342102931250010E-16, -1.000000000000000000, 0.000000000000000000 ) ) ;
#7859=CARTESIAN_POINT ( 'NONE',  ( -0.5500000000000000444, 0.5999999999999999778, 1.600000000000000089 ) ) ;
#7861=AXIS2_PLACEMENT_3D ( 'NONE', #2536, #2260, #13836 ) ;
#7862=EDGE_LOOP ( 'NONE', ( #16376, #9773, #15858, #1808, #10811, #9041 ) ) ;
#7876=ORIENTED_EDGE ( 'NONE', *, *, #16540, .T. ) ;
#7880=EDGE_LOOP ( 'NONE', ( #17857, #5694, #16595, #16233 ) ) ;
#7882=DIRECTION ( 'NONE',  ( 0.000000000000000000, -7.930164461608259947E-17, 1.000000000000000000 ) ) ;
#7887=AXIS2_PLACEMENT_3D ( 'NONE', #17960, #3902, #12431 ) ;
#7889=VECTOR ( 'NONE', #550, 1000.000000000000000 ) ;
#7901=AXIS2_PLACEMENT_3D ( 'NONE', #18095, #5530, #15363 ) ;
#7903=VECTOR ( 'NONE', #15875, 1000.000000000000000 ) ;
#7904=VERTEX_POINT ( 'NONE', #5087 ) ;
#7928=EDGE_CURVE ( 'NONE', #8163, #6491, #2423, .T. ) ;
#7933=CARTESIAN_POINT ( 'NONE',  ( 1.250000000000000000, 6.144112549695430303, 5.100000000000000533 ) ) ;
#7934=DIRECTION ( 'NONE',  ( 0.000000000000000000, -1.000000000000000000, 0.000000000000000000 ) ) ;
#7937=EDGE_LOOP ( 'NONE', ( #10361, #3166, #6544, #8863 ) ) ;
#7938=AXIS2_PLACEMENT_3D ( 'NONE', #5611, #1442, #57 ) ;
#7942=LINE ( 'NONE', #3755, #9978 ) ;
#7954=AXIS2_PLACEMENT_3D ( 'NONE', #592, #5026, #11891 ) ;
#7958=CARTESIAN_POINT ( 'NONE',  ( -1.399999999999999911, -8.000000000000000000, 6.100000000000000533 ) ) ;
#7963=VECTOR ( 'NONE', #1600, 1000.000000000000000 ) ;
#7968=LINE ( 'NONE', #1016, #1714 ) ;
#7979=DIRECTION ( 'NONE',  ( 0.000000000000000000, -1.000000000000000000, 0.000000000000000000 ) ) ;
#7981=LINE ( 'NONE', #15294, #2952 ) ;
#7984=CARTESIAN_POINT ( 'NONE',  ( -0.4000000000000000222, 2.399999999999999911, 5.100000000000000533 ) ) ;
#7990=CARTESIAN_POINT ( 'NONE',  ( 1.399999999999999911, -6.000000000000000000, 5.100000000000000533 ) ) ;
#7992=CARTESIAN_POINT ( 'NONE',  ( -1.250000000000000000, 3.881370849898470254, 5.100000000000000533 ) ) ;
#8017=EDGE_CURVE ( 'NONE', #6927, #1371, #1290, .T. ) ;
#8038=CARTESIAN_POINT ( 'NONE',  ( -1.399999999999999911, -5.000000000000000000, 6.100000000000000533 ) ) ;
#8042=ORIENTED_EDGE ( 'NONE', *, *, #11868, .T. ) ;
#8044=ADVANCED_FACE ( 'NONE', ( #10244 ), #3313, .T. ) ;
#8054=DIRECTION ( 'NONE',  ( 0.000000000000000000, -8.881784197001250351E-16, 1.000000000000000000 ) ) ;
#8055=DIRECTION ( 'NONE',  ( 0.000000000000000000, 0.000000000000000000, 1.000000000000000000 ) ) ;
#8060=ORIENTED_EDGE ( 'NONE', *, *, #10369, .T. ) ;
#8064=CARTESIAN_POINT ( 'NONE',  ( 0.5000000000000000000, 3.500000000000000000, 5.100000000000000533 ) ) ;
#8082=UNCERTAINTY_MEASURE_WITH_UNIT (LENGTH_MEASURE( 1.000000000000000082E-05 ), #4521, 'distance_accuracy_value', 'NONE');
#8102=VERTEX_POINT ( 'NONE', #15818 ) ;
#8111=ORIENTED_EDGE ( 'NONE', *, *, #1546, .F. ) ;
#8113=DIRECTION ( 'NONE',  ( 1.224646799147350002E-16, -1.000000000000000000, -6.123233995736769734E-17 ) ) ;
#8117=CARTESIAN_POINT ( 'NONE',  ( 1.399999999999999911, -5.500000000000000000, 6.100000000000000533 ) ) ;
#8119=ORIENTED_EDGE ( 'NONE', *, *, #8960, .F. ) ;
#8124=ORIENTED_EDGE ( 'NONE', *, *, #11516, .F. ) ;
#8134=EDGE_CURVE ( 'NONE', #5195, #1875, #17459, .T. ) ;
#8142=LINE ( 'NONE', #17746, #12718 ) ;
#8144=ORIENTED_EDGE ( 'NONE', *, *, #7245, .T. ) ;
#8152=FACE_OUTER_BOUND ( 'NONE', #16676, .T. ) ;
#8159=ORIENTED_EDGE ( 'NONE', *, *, #2958, .T. ) ;
#8163=VERTEX_POINT ( 'NONE', #4868 ) ;
#8171=DIRECTION ( 'NONE',  ( 2.220446049250309876E-16, -1.000000000000000000, 0.000000000000000000 ) ) ;
#8177=EDGE_LOOP ( 'NONE', ( #8987, #236, #17044, #816 ) ) ;
#8190=CARTESIAN_POINT ( 'NONE',  ( -0.5500000000000000444, 0.5999999999999999778, 1.600000000000000089 ) ) ;
#8191=DIRECTION ( 'NONE',  ( 1.110223024625159992E-16, 0.000000000000000000, -1.000000000000000000 ) ) ;
#8192=LINE ( 'NONE', #8295, #17119 ) ;
#8196=ORIENTED_EDGE ( 'NONE', *, *, #11077, .F. ) ;
#8207=ORIENTED_EDGE ( 'NONE', *, *, #11733, .T. ) ;
#8214=VECTOR ( 'NONE', #8664, 1000.000000000000000 ) ;
#8217=CARTESIAN_POINT ( 'NONE',  ( -1.000000000000000000, -7.000000000000000000, 5.700000000000000178 ) ) ;
#8221=CARTESIAN_POINT ( 'NONE',  ( -4.555459529529310125E-17, 5.131370849898479136, 6.100000000000000533 ) ) ;
#8242=AXIS2_PLACEMENT_3D ( 'NONE', #12053, #1867, #7516 ) ;
#8244=CARTESIAN_POINT ( 'NONE',  ( -0.5500000000000000444, -2.399999999999999911, 3.600000000000000089 ) ) ;
#8258=CARTESIAN_POINT ( 'NONE',  ( -8.881784197001250351E-16, 5.131370849898479136, 6.100000000000000533 ) ) ;
#8290=VECTOR ( 'NONE', #12571, 1000.000000000000000 ) ;
#8295=CARTESIAN_POINT ( 'NONE',  ( 1.399999999999999911, -5.500000000000000000, 5.100000000000000533 ) ) ;
#8299=ORIENTED_EDGE ( 'NONE', *, *, #4595, .F. ) ;
#8301=DIRECTION ( 'NONE',  ( 1.224646799147350002E-16, -1.000000000000000000, -6.123233995736769734E-17 ) ) ;
#8308=VERTEX_POINT ( 'NONE', #6233 ) ;
#8338=DIRECTION ( 'NONE',  ( 0.000000000000000000, 0.7492686492653550800, -0.6622661785325221206 ) ) ;
#8339=PLANE ( 'NONE',  #5542 ) ;
#8345=LINE ( 'NONE', #1299, #10946 ) ;
#8350=VERTEX_POINT ( 'NONE', #13178 ) ;
#8353=ORIENTED_EDGE ( 'NONE', *, *, #16840, .T. ) ;
#8364=EDGE_CURVE ( 'NONE', #3530, #1479, #16139, .T. ) ;
#8373=ORIENTED_EDGE ( 'NONE', *, *, #15264, .T. ) ;
#8376=VERTEX_POINT ( 'NONE', #10683 ) ;
#8379=ORIENTED_EDGE ( 'NONE', *, *, #3843, .F. ) ;
#8384=DIRECTION ( 'NONE',  ( -0.000000000000000000, 1.000000000000000000, 0.000000000000000000 ) ) ;
#8403=CARTESIAN_POINT ( 'NONE',  ( -0.4000000000000000222, 2.399999999999999911, 5.100000000000000533 ) ) ;
#8415=VERTEX_POINT ( 'NONE', #16235 ) ;
#8416=CARTESIAN_POINT ( 'NONE',  ( -0.4058874503045720172, 7.799999999999999822, 6.100000000000000533 ) ) ;
#8423=( BOUNDED_CURVE ( )  B_SPLINE_CURVE ( 3, ( #15700, #4111, #15432, #4387 ),
 .UNSPECIFIED., .F., .F. ) 
 B_SPLINE_CURVE_WITH_KNOTS ( ( 4, 4 ),
 ( 0.000000000000000000, 1.000000000000000000 ),
 .UNSPECIFIED. ) 
 CURVE ( )  GEOMETRIC_REPRESENTATION_ITEM ( )  RATIONAL_B_SPLINE_CURVE ( ( 1.000000000000000000, 0.8047378541243649375, 0.8047378541243649375, 1.000000000000000000 ) ) 
 REPRESENTATION_ITEM ( '' )  );
#8428=CARTESIAN_POINT ( 'NONE',  ( 1.399999999999999911, -8.000000000000000000, 3.299999999999999822 ) ) ;
#8435=DIRECTION ( 'NONE',  ( 0.000000000000000000, -1.000000000000000000, 0.000000000000000000 ) ) ;
#8449=DIRECTION ( 'NONE',  ( 0.000000000000000000, -1.000000000000000000, 0.000000000000000000 ) ) ;
#8455=ADVANCED_FACE ( 'NONE', ( #4254 ), #373, .F. ) ;
#8467=CARTESIAN_POINT ( 'NONE',  ( 0.5000000000000000000, 3.500000000000000000, 5.100000000000000533 ) ) ;
#8476=PLANE ( 'NONE',  #6434 ) ;
#8480=ORIENTED_EDGE ( 'NONE', *, *, #10102, .F. ) ;
#8503=VECTOR ( 'NONE', #5818, 1000.000000000000000 ) ;
#8509=CIRCLE ( 'NONE', #17070, 0.4000000000000000222 ) ;
#8515=DIRECTION ( 'NONE',  ( -1.000000000000000000, -1.746418240983389920E-16, -1.110223024625159992E-16 ) ) ;
#8517=LINE ( 'NONE', #14167, #14998 ) ;
#8522=FACE_OUTER_BOUND ( 'NONE', #7937, .T. ) ;
#8531=VERTEX_POINT ( 'NONE', #14071 ) ;
#8556=DIRECTION ( 'NONE',  ( 0.7071067811865480168, 0.7071067811865470176, 0.000000000000000000 ) ) ;
#8561=VERTEX_POINT ( 'NONE', #5666 ) ;
#8569=CARTESIAN_POINT ( 'NONE',  ( 1.399999999999999911, 0.5999999999999999778, 3.299999999999999822 ) ) ;
#8577=EDGE_CURVE ( 'NONE', #10029, #4545, #14267, .T. ) ;
#8583=LINE ( 'NONE', #9968, #5820 ) ;
#8588=VERTEX_POINT ( 'NONE', #104 ) ;
#8594=DIRECTION ( 'NONE',  ( 0.000000000000000000, 6.123233995736769734E-17, -1.000000000000000000 ) ) ;
#8598=ADVANCED_FACE ( 'NONE', ( #1394 ), #12702, .T. ) ;
#8612=FACE_OUTER_BOUND ( 'NONE', #9412, .T. ) ;
#8620=CARTESIAN_POINT ( 'NONE',  ( -0.4058874503045720172, 7.799999999999999822, 6.100000000000000533 ) ) ;
#8624=VERTEX_POINT ( 'NONE', #7678 ) ;
#8648=ADVANCED_FACE ( 'NONE', ( #16291 ), #10444, .F. ) ;
#8655=CARTESIAN_POINT ( 'NONE',  ( -7.347880794884118997E-17, 0.5999999999999999778, 3.673940397442059498E-17 ) ) ;
#8657=LINE ( 'NONE', #14307, #12158 ) ;
#8664=DIRECTION ( 'NONE',  ( 0.000000000000000000, -1.000000000000000000, 0.000000000000000000 ) ) ;
#8676=ORIENTED_EDGE ( 'NONE', *, *, #5942, .T. ) ;
#8692=STYLED_ITEM ( 'NONE', ( #14068 ), #1903 ) ;
#8695=EDGE_CURVE ( 'NONE', #14203, #1528, #14810, .T. ) ;
#8717=CARTESIAN_POINT ( 'NONE',  ( -1.399999999999999911, 0.5999999999999999778, 6.100000000000000533 ) ) ;
#8724=CARTESIAN_POINT ( 'NONE',  ( 0.9000000000000000222, -10.00000000000000000, 3.799999999999999822 ) ) ;
#8761=LINE ( 'NONE', #346, #10591 ) ;
#8771=ORIENTED_EDGE ( 'NONE', *, *, #14236, .T. ) ;
#8772=VECTOR ( 'NONE', #11248, 1000.000000000000000 ) ;
#8778=DIRECTION ( 'NONE',  ( -1.000000000000000000, 4.906538933386810061E-16, 0.000000000000000000 ) ) ;
#8785=VECTOR ( 'NONE', #1505, 1000.000000000000000 ) ;
#8789=ADVANCED_FACE ( 'NONE', ( #457, #4608 ), #10263, .T. ) ;
#8793=EDGE_CURVE ( 'NONE', #13096, #16755, #4054, .T. ) ;
#8794=AXIS2_PLACEMENT_3D ( 'NONE', #15318, #18055, #8449 ) ;
#8802=VECTOR ( 'NONE', #5155, 1000.000000000000000 ) ;
#8812=DIRECTION ( 'NONE',  ( -1.000000000000000000, 0.000000000000000000, 0.000000000000000000 ) ) ;
#8818=VECTOR ( 'NONE', #3148, 1000.000000000000000 ) ;
#8825=VECTOR ( 'NONE', #3029, 1000.000000000000000 ) ;
#8829=ORIENTED_EDGE ( 'NONE', *, *, #11113, .F. ) ;
#8840=DIRECTION ( 'NONE',  ( -1.224646799147350002E-16, 1.000000000000000000, 6.123233995736769734E-17 ) ) ;
#8841=VECTOR ( 'NONE', #7243, 1000.000000000000000 ) ;
#8849=ORIENTED_EDGE ( 'NONE', *, *, #662, .F. ) ;
#8855=DIRECTION ( 'NONE',  ( -0.7071067811865470176, 0.7071067811865480168, 0.000000000000000000 ) ) ;
#8857=FACE_OUTER_BOUND ( 'NONE', #6189, .T. ) ;
#8858=VECTOR ( 'NONE', #5856, 1000.000000000000000 ) ;
#8861=CARTESIAN_POINT ( 'NONE',  ( 6.858022075225179538E-16, -5.000000000000000000, -3.061616997868380183E-16 ) ) ;
#8863=ORIENTED_EDGE ( 'NONE', *, *, #9253, .F. ) ;
#8864=ADVANCED_FACE ( 'NONE', ( #11095 ), #15278, .F. ) ;
#8877=CARTESIAN_POINT ( 'NONE',  ( 1.250000000000000000, 0.5999999999999999778, 7.599999999999999645 ) ) ;
#8881=LINE ( 'NONE', #4607, #13210 ) ;
#8899=ORIENTED_EDGE ( 'NONE', *, *, #14645, .F. ) ;
#8926=ADVANCED_FACE ( 'NONE', ( #1287 ), #17230, .F. ) ;
#8942=VECTOR ( 'NONE', #6899, 1000.000000000000000 ) ;
#8960=EDGE_CURVE ( 'NONE', #14738, #8102, #4620, .T. ) ;
#8968=DIRECTION ( 'NONE',  ( 0.5521576303742329328, -0.5521576303742328218, -0.6246950475544241765 ) ) ;
#8970=ORIENTED_EDGE ( 'NONE', *, *, #2371, .F. ) ;
#8987=ORIENTED_EDGE ( 'NONE', *, *, #16310, .F. ) ;
#8991=EDGE_CURVE ( 'NONE', #14727, #8163, #4530, .T. ) ;
#8994=LINE ( 'NONE', #13089, #5850 ) ;
#8997=ORIENTED_EDGE ( 'NONE', *, *, #13676, .T. ) ;
#9011=CARTESIAN_POINT ( 'NONE',  ( 1.399999999999999911, 0.5999999999999999778, 3.299999999999999822 ) ) ;
#9014=DIRECTION ( 'NONE',  ( -2.467162276944790449E-16, 0.000000000000000000, -1.000000000000000000 ) ) ;
#9027=LINE ( 'NONE', #9123, #7595 ) ;
#9031=VECTOR ( 'NONE', #2870, 1000.000000000000000 ) ;
#9041=ORIENTED_EDGE ( 'NONE', *, *, #14794, .F. ) ;
#9042=AXIS2_PLACEMENT_3D ( 'NONE', #1619, #17318, #2922 ) ;
#9044=CARTESIAN_POINT ( 'NONE',  ( -0.9000000000000000222, -10.00000000000000000, 3.799999999999999822 ) ) ;
#9049=EDGE_CURVE ( 'NONE', #7321, #11273, #14192, .T. ) ;
#9054=LINE ( 'NONE', #10449, #14143 ) ;
#9061=AXIS2_PLACEMENT_3D ( 'NONE', #9510, #15167, #9595 ) ;
#9071=ORIENTED_EDGE ( 'NONE', *, *, #4503, .T. ) ;
#9072=VECTOR ( 'NONE', #16911, 1000.000000000000000 ) ;
#9089=DIRECTION ( 'NONE',  ( -0.7071067811865470176, 0.7071067811865480168, 0.000000000000000000 ) ) ;
#9099=VECTOR ( 'NONE', #5964, 1000.000000000000000 ) ;
#9107=EDGE_CURVE ( 'NONE', #13986, #16755, #4263, .T. ) ;
#9123=CARTESIAN_POINT ( 'NONE',  ( 0.5500000000000000444, 7.799999999999999822, 3.600000000000000089 ) ) ;
#9132=EDGE_CURVE ( 'NONE', #8588, #6816, #7423, .T. ) ;
#9136=DIRECTION ( 'NONE',  ( -1.000000000000000000, 0.000000000000000000, 0.000000000000000000 ) ) ;
#9137=EDGE_CURVE ( 'NONE', #7321, #5031, #14276, .T. ) ;
#9140=EDGE_CURVE ( 'NONE', #8561, #2147, #201, .T. ) ;
#9146=EDGE_LOOP ( 'NONE', ( #1232, #7601, #2578, #14471, #5024, #15443, #17172, #10844 ) ) ;
#9149=ORIENTED_EDGE ( 'NONE', *, *, #5414, .F. ) ;
#9150=VECTOR ( 'NONE', #13961, 1000.000000000000000 ) ;
#9168=ORIENTED_EDGE ( 'NONE', *, *, #17393, .F. ) ;
#9176=VECTOR ( 'NONE', #3018, 1000.000000000000000 ) ;
#9207=DIRECTION ( 'NONE',  ( 0.000000000000000000, 0.000000000000000000, -1.000000000000000000 ) ) ;
#9221=AXIS2_PLACEMENT_3D ( 'NONE', #12498, #8515, #13889 ) ;
#9231=DIRECTION ( 'NONE',  ( -1.665334536937729880E-16, 0.000000000000000000, -1.000000000000000000 ) ) ;
#9235=DIRECTION ( 'NONE',  ( -1.000000000000000000, 0.000000000000000000, 0.000000000000000000 ) ) ;
#9238=LINE ( 'NONE', #16287, #12836 ) ;
#9240=DIRECTION ( 'NONE',  ( 0.000000000000000000, -1.000000000000000000, -8.881784197001250351E-16 ) ) ;
#9244=VECTOR ( 'NONE', #15988, 1000.000000000000000 ) ;
#9253=EDGE_CURVE ( 'NONE', #10029, #851, #6638, .T. ) ;
#9264=ORIENTED_EDGE ( 'NONE', *, *, #12422, .T. ) ;
#9287=ORIENTED_EDGE ( 'NONE', *, *, #5182, .T. ) ;
#9303=CARTESIAN_POINT ( 'NONE',  ( 0.5500000000000000444, 6.450000000000000178, 1.600000000000000089 ) ) ;
#9307=DIRECTION ( 'NONE',  ( 0.000000000000000000, 3.965082230804129973E-17, -1.000000000000000000 ) ) ;
#9308=FACE_OUTER_BOUND ( 'NONE', #6352, .T. ) ;
#9309=CARTESIAN_POINT ( 'NONE',  ( -1.800000000000000044, 7.799999999999999822, 1.600000000000000089 ) ) ;
#9321=VERTEX_POINT ( 'NONE', #13600 ) ;
#9322=FACE_OUTER_BOUND ( 'NONE', #3468, .T. ) ;
#9360=CIRCLE ( 'NONE', #12925, 0.5000000000000004441 ) ;
#9388=VERTEX_POINT ( 'NONE', #4849 ) ;
#9395=VECTOR ( 'NONE', #12475, 1000.000000000000000 ) ;
#9398=DIRECTION ( 'NONE',  ( 1.306144734853129823E-16, 6.530723674265629391E-17, -1.000000000000000000 ) ) ;
#9408=ORIENTED_EDGE ( 'NONE', *, *, #15171, .T. ) ;
#9412=EDGE_LOOP ( 'NONE', ( #14560, #16412, #10258, #1901 ) ) ;
#9416=LINE ( 'NONE', #13299, #2612 ) ;
#9417=DIRECTION ( 'NONE',  ( -1.000000000000000000, 2.220446049250310320E-15, 0.000000000000000000 ) ) ;
#9431=EDGE_LOOP ( 'NONE', ( #14311, #11969, #16293, #6230, #9858, #11372 ) ) ;
#9432=EDGE_CURVE ( 'NONE', #458, #1463, #15893, .T. ) ;
#9465=DIRECTION ( 'NONE',  ( -2.220446049250309876E-16, 0.000000000000000000, 1.000000000000000000 ) ) ;
#9491=CARTESIAN_POINT ( 'NONE',  ( 1.250000000000000000, 0.5999999999999999778, 6.100000000000000533 ) ) ;
#9497=ORIENTED_EDGE ( 'NONE', *, *, #15225, .F. ) ;
#9500=DIRECTION ( 'NONE',  ( 7.930164461608259947E-17, -1.000000000000000000, 0.000000000000000000 ) ) ;
#9510=CARTESIAN_POINT ( 'NONE',  ( -1.399999999999999911, -8.000000000000000000, 3.299999999999999822 ) ) ;
#9522=CARTESIAN_POINT ( 'NONE',  ( 1.000000000000000000, -7.000000000000000000, 5.700000000000000178 ) ) ;
#9526=DIRECTION ( 'NONE',  ( 2.168404344971006896E-16, -1.000000000000000000, 0.000000000000000000 ) ) ;
#9540=CARTESIAN_POINT ( 'NONE',  ( 0.9000000000000000222, 2.050000000000000266, 3.600000000000000089 ) ) ;
#9562=ORIENTED_EDGE ( 'NONE', *, *, #2371, .T. ) ;
#9587=ORIENTED_EDGE ( 'NONE', *, *, #881, .F. ) ;
#9590=ORIENTED_EDGE ( 'NONE', *, *, #14135, .F. ) ;
#9592=CARTESIAN_POINT ( 'NONE',  ( -1.399999999999999911, -9.500000000000000000, 6.100000000000000533 ) ) ;
#9595=DIRECTION ( 'NONE',  ( 0.000000000000000000, -1.000000000000000000, 0.000000000000000000 ) ) ;
#9606=LINE ( 'NONE', #6920, #3493 ) ;
#9610=DIRECTION ( 'NONE',  ( 1.000000000000000000, 1.224646799147350002E-16, 0.000000000000000000 ) ) ;
#9612=VERTEX_POINT ( 'NONE', #12179 ) ;
#9613=VECTOR ( 'NONE', #11708, 1000.000000000000000 ) ;
#9614=EDGE_CURVE ( 'NONE', #16401, #2785, #16535, .T. ) ;
#9615=VERTEX_POINT ( 'NONE', #14836 ) ;
#9639=AXIS2_PLACEMENT_3D ( 'NONE', #8064, #17931, #10927 ) ;
#9651=EDGE_LOOP ( 'NONE', ( #10959, #14375, #14160, #12591 ) ) ;
#9666=CARTESIAN_POINT ( 'NONE',  ( 0.5500000000000000444, 6.450000000000000178, 3.600000000000000089 ) ) ;
#9686=AXIS2_PLACEMENT_3D ( 'NONE', #4132, #15361, #6915 ) ;
#9698=AXIS2_PLACEMENT_3D ( 'NONE', #12183, #8113, #6715 ) ;
#9703=FACE_OUTER_BOUND ( 'NONE', #10732, .T. ) ;
#9717=CARTESIAN_POINT ( 'NONE',  ( -1.000000000000000000, -6.000000000000000000, 3.299999999999999822 ) ) ;
#9721=EDGE_CURVE ( 'NONE', #4438, #12426, #14536, .T. ) ;
#9724=VECTOR ( 'NONE', #5761, 1000.000000000000000 ) ;
#9730=ORIENTED_EDGE ( 'NONE', *, *, #11085, .T. ) ;
#9732=DIRECTION ( 'NONE',  ( -1.000000000000000000, 0.000000000000000000, 0.000000000000000000 ) ) ;
#9746=CARTESIAN_POINT ( 'NONE',  ( 0.5500000000000000444, 2.050000000000000266, 3.600000000000000089 ) ) ;
#9761=ORIENTED_EDGE ( 'NONE', *, *, #9137, .T. ) ;
#9769=LINE ( 'NONE', #15236, #8772 ) ;
#9772=DIRECTION ( 'NONE',  ( 1.000000000000000000, 4.037174635000560229E-16, 0.000000000000000000 ) ) ;
#9773=ORIENTED_EDGE ( 'NONE', *, *, #11516, .T. ) ;
#9775=FACE_OUTER_BOUND ( 'NONE', #16340, .T. ) ;
#9807=ORIENTED_EDGE ( 'NONE', *, *, #8991, .F. ) ;
#9822=EDGE_CURVE ( 'NONE', #9877, #8376, #14883, .T. ) ;
#9824=ORIENTED_EDGE ( 'NONE', *, *, #10473, .F. ) ;
#9833=CARTESIAN_POINT ( 'NONE',  ( -0.5500000000000000444, 7.799999999999999822, 3.600000000000000089 ) ) ;
#9858=ORIENTED_EDGE ( 'NONE', *, *, #9955, .F. ) ;
#9859=DIRECTION ( 'NONE',  ( 1.000000000000000000, 0.000000000000000000, 0.000000000000000000 ) ) ;
#9865=ORIENTED_EDGE ( 'NONE', *, *, #6265, .T. ) ;
#9877=VERTEX_POINT ( 'NONE', #3665 ) ;
#9903=DIRECTION ( 'NONE',  ( 0.000000000000000000, -1.000000000000000000, 0.000000000000000000 ) ) ;
#9913=ORIENTED_EDGE ( 'NONE', *, *, #13766, .T. ) ;
#9917=CARTESIAN_POINT ( 'NONE',  ( 1.800000000000000044, 0.5999999999999999778, 1.600000000000000089 ) ) ;
#9919=FACE_OUTER_BOUND ( 'NONE', #17880, .T. ) ;
#9941=ORIENTED_EDGE ( 'NONE', *, *, #13069, .F. ) ;
#9948=DIRECTION ( 'NONE',  ( 1.000000000000000000, 0.000000000000000000, 0.000000000000000000 ) ) ;
#9952=VERTEX_POINT ( 'NONE', #15519 ) ;
#9955=EDGE_CURVE ( 'NONE', #5117, #6801, #2540, .T. ) ;
#9959=CARTESIAN_POINT ( 'NONE',  ( 6.429395695523600208E-16, 3.500000000000000000, 5.100000000000000533 ) ) ;
#9962=ORIENTED_EDGE ( 'NONE', *, *, #9137, .F. ) ;
#9968=CARTESIAN_POINT ( 'NONE',  ( 0.5000000000000000000, 3.500000000000000000, 6.100000000000000533 ) ) ;
#9976=EDGE_CURVE ( 'NONE', #851, #2878, #8192, .T. ) ;
#9978=VECTOR ( 'NONE', #9417, 1000.000000000000000 ) ;
#9987=ORIENTED_EDGE ( 'NONE', *, *, #14723, .T. ) ;
#10029=VERTEX_POINT ( 'NONE', #15611 ) ;
#10041=ADVANCED_FACE ( 'NONE', ( #16703 ), #15433, .F. ) ;
#10057=AXIS2_PLACEMENT_3D ( 'NONE', #12215, #7854, #10728 ) ;
#10065=EDGE_CURVE ( 'NONE', #7652, #13315, #7249, .T. ) ;
#10072=LINE ( 'NONE', #4762, #1441 ) ;
#10097=DIRECTION ( 'NONE',  ( 0.000000000000000000, 0.000000000000000000, 1.000000000000000000 ) ) ;
#10102=EDGE_CURVE ( 'NONE', #15567, #5243, #17133, .T. ) ;
#10109=CARTESIAN_POINT ( 'NONE',  ( 0.9000000000000000222, 6.450000000000000178, 1.600000000000000089 ) ) ;
#10120=EDGE_LOOP ( 'NONE', ( #478, #4631, #9941, #8299 ) ) ;
#10129=CARTESIAN_POINT ( 'NONE',  ( 1.250000000000000000, 0.5999999999999999778, 6.100000000000000533 ) ) ;
#10147=DIRECTION ( 'NONE',  ( -1.531342102931250010E-16, 1.000000000000000000, 0.000000000000000000 ) ) ;
#10187=CARTESIAN_POINT ( 'NONE',  ( 1.399999999999999911, -7.000000000000000000, 6.100000000000000533 ) ) ;
#10203=FACE_OUTER_BOUND ( 'NONE', #4522, .T. ) ;
#10219=VERTEX_POINT ( 'NONE', #14197 ) ;
#10228=CARTESIAN_POINT ( 'NONE',  ( -1.250000000000000000, 3.500000000000000000, 5.100000000000000533 ) ) ;
#10237=FACE_OUTER_BOUND ( 'NONE', #13129, .T. ) ;
#10243=EDGE_CURVE ( 'NONE', #2335, #5031, #14285, .T. ) ;
#10244=FACE_OUTER_BOUND ( 'NONE', #12892, .T. ) ;
#10245=LINE ( 'NONE', #171, #6714 ) ;
#10250=DIRECTION ( 'NONE',  ( 0.000000000000000000, 0.000000000000000000, 1.000000000000000000 ) ) ;
#10252=PLANE ( 'NONE',  #17023 ) ;
#10258=ORIENTED_EDGE ( 'NONE', *, *, #13431, .F. ) ;
#10259=CARTESIAN_POINT ( 'NONE',  ( -1.399999999999999911, -9.500000000000000000, 3.299999999999999822 ) ) ;
#10261=DIRECTION ( 'NONE',  ( -1.000000000000000000, -1.306144734853119962E-16, 0.000000000000000000 ) ) ;
#10263=PLANE ( 'NONE',  #3203 ) ;
#10271=EDGE_CURVE ( 'NONE', #6491, #9952, #11866, .T. ) ;
#10277=EDGE_CURVE ( 'NONE', #5830, #10219, #16115, .T. ) ;
#10279=CARTESIAN_POINT ( 'NONE',  ( -1.250000000000000000, 7.799999999999999822, 5.100000000000000533 ) ) ;
#10281=EDGE_CURVE ( 'NONE', #1367, #5117, #17298, .T. ) ;
#10285=CARTESIAN_POINT ( 'NONE',  ( -1.800000000000000044, 0.5999999999999999778, 1.600000000000000089 ) ) ;
#10313=CARTESIAN_POINT ( 'NONE',  ( 1.000000000000000000, -7.000000000000000000, 3.700000000000000178 ) ) ;
#10314=VECTOR ( 'NONE', #2896, 1000.000000000000000 ) ;
#10316=ORIENTED_EDGE ( 'NONE', *, *, #5074, .T. ) ;
#10356=ORIENTED_EDGE ( 'NONE', *, *, #8793, .T. ) ;
#10361=ORIENTED_EDGE ( 'NONE', *, *, #4770, .T. ) ;
#10369=EDGE_CURVE ( 'NONE', #14203, #10460, #10549, .T. ) ;
#10377=EDGE_CURVE ( 'NONE', #2805, #13228, #4534, .T. ) ;
#10391=CARTESIAN_POINT ( 'NONE',  ( 1.399999999999999911, -6.000000000000000000, 3.299999999999999822 ) ) ;
#10411=DIRECTION ( 'NONE',  ( 0.000000000000000000, 0.000000000000000000, 1.000000000000000000 ) ) ;
#10424=( NAMED_UNIT ( * ) SI_UNIT ( $, .STERADIAN. ) SOLID_ANGLE_UNIT ( ) );
#10439=ORIENTED_EDGE ( 'NONE', *, *, #5373, .T. ) ;
#10444=PLANE ( 'NONE',  #15344 ) ;
#10449=CARTESIAN_POINT ( 'NONE',  ( 6.661338147750939243E-16, 3.500000000000000000, 5.100000000000000533 ) ) ;
#10460=VERTEX_POINT ( 'NONE', #6577 ) ;
#10467=PLANE ( 'NONE',  #14119 ) ;
#10473=EDGE_CURVE ( 'NONE', #4745, #4957, #6484, .T. ) ;
#10487=EDGE_CURVE ( 'NONE', #5830, #6456, #7981, .T. ) ;
#10498=DIRECTION ( 'NONE',  ( 2.960594732333750117E-16, -1.000000000000000000, 0.000000000000000000 ) ) ;
#10509=DIRECTION ( 'NONE',  ( 1.000000000000000000, 0.000000000000000000, 0.000000000000000000 ) ) ;
#10510=ORIENTED_EDGE ( 'NONE', *, *, #8134, .F. ) ;
#10511=DIRECTION ( 'NONE',  ( 1.110223024625159992E-16, -1.000000000000000000, 0.000000000000000000 ) ) ;
#10520=ORIENTED_EDGE ( 'NONE', *, *, #14277, .F. ) ;
#10521=LINE ( 'NONE', #13405, #4084 ) ;
#10525=ORIENTED_EDGE ( 'NONE', *, *, #11105, .T. ) ;
#10533=EDGE_LOOP ( 'NONE', ( #16073, #14854, #3115, #14588 ) ) ;
#10536=EDGE_CURVE ( 'NONE', #16922, #1039, #12696, .T. ) ;
#10541=VECTOR ( 'NONE', #14487, 1000.000000000000000 ) ;
#10549=LINE ( 'NONE', #14627, #1176 ) ;
#10557=VECTOR ( 'NONE', #17523, 1000.000000000000000 ) ;
#10558=ORIENTED_EDGE ( 'NONE', *, *, #1573, .F. ) ;
#10568=DIRECTION ( 'NONE',  ( 1.224646799147350002E-16, -1.000000000000000000, -6.123233995736769734E-17 ) ) ;
#10583=EDGE_CURVE ( 'NONE', #14447, #1528, #2693, .T. ) ;
#10586=ORIENTED_EDGE ( 'NONE', *, *, #6878, .T. ) ;
#10591=VECTOR ( 'NONE', #10147, 1000.000000000000000 ) ;
#10593=AXIS2_PLACEMENT_3D ( 'NONE', #1589, #4346, #4442 ) ;
#10594=DIRECTION ( 'NONE',  ( 0.000000000000000000, 0.000000000000000000, 1.000000000000000000 ) ) ;
#10606=EDGE_CURVE ( 'NONE', #6296, #4438, #8345, .T. ) ;
#10610=EDGE_CURVE ( 'NONE', #15567, #6801, #1493, .T. ) ;
#10616=LINE ( 'NONE', #16265, #4625 ) ;
#10619=EDGE_CURVE ( 'NONE', #1479, #305, #6943, .T. ) ;
#10639=EDGE_CURVE ( 'NONE', #15319, #15809, #5564, .T. ) ;
#10645=APPLICATION_CONTEXT ( 'automotive_design' ) ;
#10667=LINE ( 'NONE', #5105, #15127 ) ;
#10668=PRODUCT_CONTEXT ( 'NONE', #10645, 'mechanical' ) ;
#10683=CARTESIAN_POINT ( 'NONE',  ( -1.000000000000000000, -8.000000000000000000, 3.700000000000000178 ) ) ;
#10691=LINE ( 'NONE', #6518, #18194 ) ;
#10692=DIRECTION ( 'NONE',  ( -0.7071067811865480168, 0.7071067811865470176, 0.000000000000000000 ) ) ;
#10694=DIRECTION ( 'NONE',  ( 1.000000000000000000, 1.233581138472399909E-16, 1.480297366166879989E-16 ) ) ;
#10709=DIRECTION ( 'NONE',  ( 1.000000000000000000, 1.224646799147350002E-16, 0.000000000000000000 ) ) ;
#10728=DIRECTION ( 'NONE',  ( 1.000000000000000000, 0.000000000000000000, 0.000000000000000000 ) ) ;
#10732=EDGE_LOOP ( 'NONE', ( #2473, #3095, #13879, #10520, #6907, #15935, #9264, #8042 ) ) ;
#10733=FACE_OUTER_BOUND ( 'NONE', #10120, .T. ) ;
#10735=ORIENTED_EDGE ( 'NONE', *, *, #11868, .F. ) ;
#10739=CARTESIAN_POINT ( 'NONE',  ( 0.9000000000000000222, -9.500000000000000000, 1.300000000000000044 ) ) ;
#10749=CARTESIAN_POINT ( 'NONE',  ( 0.9000000000000000222, 2.050000000000000266, 1.600000000000000089 ) ) ;
#10750=DIRECTION ( 'NONE',  ( -8.397698689135169229E-17, 1.000000000000000000, 0.000000000000000000 ) ) ;
#10785=CARTESIAN_POINT ( 'NONE',  ( 0.5500000000000000444, 0.5999999999999999778, 3.299999999999999822 ) ) ;
#10811=ORIENTED_EDGE ( 'NONE', *, *, #1802, .T. ) ;
#10826=VERTEX_POINT ( 'NONE', #6188 ) ;
#10831=DIRECTION ( 'NONE',  ( 1.306144734853129823E-16, -2.378183611328045350E-31, 1.000000000000000000 ) ) ;
#10837=PLANE ( 'NONE',  #15035 ) ;
#10844=ORIENTED_EDGE ( 'NONE', *, *, #15142, .F. ) ;
#10849=VERTEX_POINT ( 'NONE', #8877 ) ;
#10857=EDGE_LOOP ( 'NONE', ( #219, #5877, #11963, #4350, #210, #2394 ) ) ;
#10898=EDGE_CURVE ( 'NONE', #11273, #13665, #2210, .T. ) ;
#10900=EDGE_LOOP ( 'NONE', ( #5958, #11282, #4312, #2957 ) ) ;
#10913=PLANE ( 'NONE',  #7901 ) ;
#10924=ORIENTED_EDGE ( 'NONE', *, *, #1802, .F. ) ;
#10927=DIRECTION ( 'NONE',  ( 0.000000000000000000, 0.000000000000000000, -1.000000000000000000 ) ) ;
#10928=DIRECTION ( 'NONE',  ( 0.000000000000000000, 0.000000000000000000, 1.000000000000000000 ) ) ;
#10939=FACE_OUTER_BOUND ( 'NONE', #4373, .T. ) ;
#10946=VECTOR ( 'NONE', #10097, 1000.000000000000000 ) ;
#10953=EDGE_CURVE ( 'NONE', #9321, #2413, #15686, .T. ) ;
#10955=VECTOR ( 'NONE', #16902, 1000.000000000000000 ) ;
#10957=ADVANCED_FACE ( 'NONE', ( #13700 ), #14995, .T. ) ;
#10959=ORIENTED_EDGE ( 'NONE', *, *, #12979, .F. ) ;
#10965=ORIENTED_EDGE ( 'NONE', *, *, #5895, .F. ) ;
#10972=DIRECTION ( 'NONE',  ( 0.000000000000000000, 0.000000000000000000, 1.000000000000000000 ) ) ;
#10976=LINE ( 'NONE', #2539, #2143 ) ;
#10980=EDGE_CURVE ( 'NONE', #2413, #8624, #8142, .T. ) ;
#10982=LINE ( 'NONE', #16629, #8942 ) ;
#10989=DIRECTION ( 'NONE',  ( -7.930164461608259947E-17, 0.000000000000000000, -1.000000000000000000 ) ) ;
#10998=LINE ( 'NONE', #16647, #7010 ) ;
#11008=CYLINDRICAL_SURFACE ( 'NONE', #6046, 0.5000000000000004441 ) ;
#11017=CARTESIAN_POINT ( 'NONE',  ( -1.000000000000000000, -5.000000000000000000, 6.100000000000000533 ) ) ;
#11027=ORIENTED_EDGE ( 'NONE', *, *, #6636, .T. ) ;
#11042=CARTESIAN_POINT ( 'NONE',  ( -1.250000000000000000, 3.881370849898470254, 5.100000000000000533 ) ) ;
#11049=VERTEX_POINT ( 'NONE', #7764 ) ;
#11061=CARTESIAN_POINT ( 'NONE',  ( 1.399999999999999911, -7.000000000000000000, 3.299999999999999822 ) ) ;
#11062=PLANE ( 'NONE',  #17357 ) ;
#11065=DIRECTION ( 'NONE',  ( 0.000000000000000000, -1.000000000000000000, -2.220446049250309876E-16 ) ) ;
#11077=EDGE_CURVE ( 'NONE', #4535, #9612, #823, .T. ) ;
#11080=LINE ( 'NONE', #13953, #9395 ) ;
#11084=LINE ( 'NONE', #16650, #12070 ) ;
#11085=EDGE_CURVE ( 'NONE', #5300, #620, #12127, .T. ) ;
#11095=FACE_OUTER_BOUND ( 'NONE', #11509, .T. ) ;
#11100=DIRECTION ( 'NONE',  ( 1.233581138472399909E-16, 6.167905692361979821E-17, -1.000000000000000000 ) ) ;
#11105=EDGE_CURVE ( 'NONE', #11415, #16121, #6924, .T. ) ;
#11108=ORIENTED_EDGE ( 'NONE', *, *, #15830, .F. ) ;
#11109=ADVANCED_FACE ( 'NONE', ( #9703 ), #4229, .F. ) ;
#11113=EDGE_CURVE ( 'NONE', #4627, #356, #78, .T. ) ;
#11114=ORIENTED_EDGE ( 'NONE', *, *, #111, .F. ) ;
#11115=LINE ( 'NONE', #4976, #7637 ) ;
#11118=AXIS2_PLACEMENT_3D ( 'NONE', #13991, #14076, #1506 ) ;
#11128=ORIENTED_EDGE ( 'NONE', *, *, #8577, .T. ) ;
#11143=ORIENTED_EDGE ( 'NONE', *, *, #5942, .F. ) ;
#11157=VECTOR ( 'NONE', #6959, 1000.000000000000000 ) ;
#11178=EDGE_CURVE ( 'NONE', #6296, #458, #1470, .T. ) ;
#11187=DIRECTION ( 'NONE',  ( -4.906538933386810061E-16, -1.000000000000000000, 0.000000000000000000 ) ) ;
#11188=ORIENTED_EDGE ( 'NONE', *, *, #10243, .T. ) ;
#11191=CARTESIAN_POINT ( 'NONE',  ( 0.000000000000000000, 0.000000000000000000, 0.000000000000000000 ) ) ;
#11200=CARTESIAN_POINT ( 'NONE',  ( 1.000000000000000000, -5.000000000000000000, 3.299999999999999822 ) ) ;
#11204=FACE_OUTER_BOUND ( 'NONE', #1253, .T. ) ;
#11213=( NAMED_UNIT ( * ) PLANE_ANGLE_UNIT ( ) SI_UNIT ( $, .RADIAN. ) );
#11218=VECTOR ( 'NONE', #3516, 1000.000000000000000 ) ;
#11230=ORIENTED_EDGE ( 'NONE', *, *, #13426, .F. ) ;
#11234=ORIENTED_EDGE ( 'NONE', *, *, #12436, .T. ) ;
#11248=DIRECTION ( 'NONE',  ( -7.930164461608259947E-17, 0.000000000000000000, -1.000000000000000000 ) ) ;
#11259=AXIS2_PLACEMENT_3D ( 'NONE', #8861, #13121, #1991 ) ;
#11273=VERTEX_POINT ( 'NONE', #5449 ) ;
#11278=CARTESIAN_POINT ( 'NONE',  ( 6.858022075225179538E-16, -5.000000000000000000, -3.061616997868380183E-16 ) ) ;
#11282=ORIENTED_EDGE ( 'NONE', *, *, #11085, .F. ) ;
#11302=EDGE_LOOP ( 'NONE', ( #4462, #750, #14246, #16023 ) ) ;
#11304=SURFACE_STYLE_FILL_AREA ( #17024 ) ;
#11305=ORIENTED_EDGE ( 'NONE', *, *, #10619, .T. ) ;
#11315=EDGE_CURVE ( 'NONE', #4745, #15319, #3377, .T. ) ;
#11353=ORIENTED_EDGE ( 'NONE', *, *, #7413, .T. ) ;
#11354=DIRECTION ( 'NONE',  ( 1.000000000000000000, 0.000000000000000000, -2.220446049250319983E-16 ) ) ;
#11358=ORIENTED_EDGE ( 'NONE', *, *, #12878, .T. ) ;
#11371=ORIENTED_EDGE ( 'NONE', *, *, #13224, .T. ) ;
#11372=ORIENTED_EDGE ( 'NONE', *, *, #7576, .F. ) ;
#11375=LINE ( 'NONE', #17097, #16207 ) ;
#11388=DIRECTION ( 'NONE',  ( 1.480297366166879989E-16, -1.000000000000000000, -1.480297366166879989E-16 ) ) ;
#11392=ADVANCED_FACE ( 'NONE', ( #17260 ), #4575, .T. ) ;
#11398=DIRECTION ( 'NONE',  ( 0.000000000000000000, -1.000000000000000000, -6.167905692361979821E-17 ) ) ;
#11415=VERTEX_POINT ( 'NONE', #16080 ) ;
#11417=ORIENTED_EDGE ( 'NONE', *, *, #11893, .F. ) ;
#11421=AXIS2_PLACEMENT_3D ( 'NONE', #12690, #17017, #4433 ) ;
#11436=DIRECTION ( 'NONE',  ( 1.000000000000000000, 1.644774851296529842E-16, 1.110223024625159992E-16 ) ) ;
#11439=ORIENTED_EDGE ( 'NONE', *, *, #10619, .F. ) ;
#11452=DIRECTION ( 'NONE',  ( 0.7071067811865470176, -0.7071067811865480168, 0.000000000000000000 ) ) ;
#11455=CARTESIAN_POINT ( 'NONE',  ( 7.069631497386979886E-16, 5.131370849898479136, 5.100000000000000533 ) ) ;
#11462=DIRECTION ( 'NONE',  ( 1.189524669241239855E-16, -1.000000000000000000, 0.000000000000000000 ) ) ;
#11481=VECTOR ( 'NONE', #15116, 1000.000000000000000 ) ;
#11482=DIRECTION ( 'NONE',  ( 0.000000000000000000, -1.000000000000000000, 0.000000000000000000 ) ) ;
#11484=DIRECTION ( 'NONE',  ( 1.000000000000000000, 1.233581138472399909E-16, 1.480297366166879989E-16 ) ) ;
#11509=EDGE_LOOP ( 'NONE', ( #15496, #9824, #13533, #3162 ) ) ;
#11515=ORIENTED_EDGE ( 'NONE', *, *, #582, .F. ) ;
#11516=EDGE_CURVE ( 'NONE', #2878, #1367, #2086, .T. ) ;
#11518=CARTESIAN_POINT ( 'NONE',  ( 1.399999999999999911, -8.000000000000000000, 6.100000000000000533 ) ) ;
#11525=ORIENTED_EDGE ( 'NONE', *, *, #7553, .F. ) ;
#11529=AXIS2_PLACEMENT_3D ( 'NONE', #15370, #2576, #9610 ) ;
#11531=ORIENTED_EDGE ( 'NONE', *, *, #5108, .F. ) ;
#11537=DIRECTION ( 'NONE',  ( -2.220446049250309876E-16, 0.000000000000000000, 1.000000000000000000 ) ) ;
#11548=DIRECTION ( 'NONE',  ( 1.000000000000000000, 0.000000000000000000, 0.000000000000000000 ) ) ;
#11565=FILL_AREA_STYLE_COLOUR ( '', #18126 ) ;
#11580=PLANE ( 'NONE',  #2900 ) ;
#11588=DIRECTION ( 'NONE',  ( 0.000000000000000000, -1.000000000000000000, -6.167905692361979821E-17 ) ) ;
#11589=VERTEX_POINT ( 'NONE', #9303 ) ;
#11591=EDGE_CURVE ( 'NONE', #4320, #12426, #6621, .T. ) ;
#11596=VERTEX_POINT ( 'NONE', #4857 ) ;
#11602=LINE ( 'NONE', #10129, #16185 ) ;
#11604=EDGE_LOOP ( 'NONE', ( #2550, #16278, #9408, #1849, #6629, #11128 ) ) ;
#11646=VECTOR ( 'NONE', #9732, 1000.000000000000000 ) ;
#11653=EDGE_CURVE ( 'NONE', #15319, #7510, #15624, .T. ) ;
#11674=EDGE_LOOP ( 'NONE', ( #1606, #1987, #12286, #10510, #6362, #15907, #10439, #15136 ) ) ;
#11681=CARTESIAN_POINT ( 'NONE',  ( -1.399999999999999911, 0.5999999999999999778, 6.100000000000000533 ) ) ;
#11696=CARTESIAN_POINT ( 'NONE',  ( 0.5500000000000000444, 2.050000000000000266, 3.600000000000000089 ) ) ;
#11701=VECTOR ( 'NONE', #13136, 1000.000000000000000 ) ;
#11708=DIRECTION ( 'NONE',  ( 2.220446049250319983E-16, 0.000000000000000000, 1.000000000000000000 ) ) ;
#11715=LINE ( 'NONE', #16074, #235 ) ;
#11721=CARTESIAN_POINT ( 'NONE',  ( 7.233457020361919865E-16, 4.000000000000000000, 5.100000000000000533 ) ) ;
#11733=EDGE_CURVE ( 'NONE', #1039, #1367, #1627, .T. ) ;
#11745=CARTESIAN_POINT ( 'NONE',  ( 1.000000000000000000, -7.000000000000000000, 5.700000000000000178 ) ) ;
#11779=ORIENTED_EDGE ( 'NONE', *, *, #3281, .T. ) ;
#11786=ORIENTED_EDGE ( 'NONE', *, *, #14794, .T. ) ;
#11793=DIRECTION ( 'NONE',  ( -0.7071067811865470176, 0.7071067811865480168, 0.000000000000000000 ) ) ;
#11809=ORIENTED_EDGE ( 'NONE', *, *, #15612, .F. ) ;
#11812=LINE ( 'NONE', #15888, #4938 ) ;
#11819=PLANE ( 'NONE',  #817 ) ;
#11829=ORIENTED_EDGE ( 'NONE', *, *, #3124, .T. ) ;
#11843=EDGE_CURVE ( 'NONE', #16255, #2694, #16060, .T. ) ;
#11849=PLANE ( 'NONE',  #12623 ) ;
#11856=DIRECTION ( 'NONE',  ( -0.7071067811865470176, 0.7071067811865480168, 0.000000000000000000 ) ) ;
#11866=LINE ( 'NONE', #4806, #11218 ) ;
#11868=EDGE_CURVE ( 'NONE', #16856, #16401, #8657, .T. ) ;
#11871=EDGE_LOOP ( 'NONE', ( #15536, #7016, #12050, #12828 ) ) ;
#11877=EDGE_CURVE ( 'NONE', #16167, #14474, #14850, .T. ) ;
#11879=CARTESIAN_POINT ( 'NONE',  ( 6.429395695523600208E-16, 3.500000000000000000, 5.100000000000000533 ) ) ;
#11883=CARTESIAN_POINT ( 'NONE',  ( 9.797174393178831574E-16, -8.000000000000000000, -4.898587196589410857E-16 ) ) ;
#11887=LINE ( 'NONE', #6397, #4364 ) ;
#11891=DIRECTION ( 'NONE',  ( 1.000000000000000000, 0.000000000000000000, 0.000000000000000000 ) ) ;
#11893=EDGE_CURVE ( 'NONE', #1463, #16167, #768, .T. ) ;
#11899=LINE ( 'NONE', #14253, #6956 ) ;
#11909=CARTESIAN_POINT ( 'NONE',  ( 8.549934884138839976E-16, 6.262741699796950279, 5.100000000000000533 ) ) ;
#11932=ORIENTED_EDGE ( 'NONE', *, *, #15225, .T. ) ;
#11934=LINE ( 'NONE', #6191, #12543 ) ;
#11937=ORIENTED_EDGE ( 'NONE', *, *, #2055, .T. ) ;
#11963=ORIENTED_EDGE ( 'NONE', *, *, #15724, .F. ) ;
#11964=EDGE_CURVE ( 'NONE', #305, #1875, #15652, .T. ) ;
#11969=ORIENTED_EDGE ( 'NONE', *, *, #9049, .T. ) ;
#11997=LINE ( 'NONE', #18241, #4781 ) ;
#12000=EDGE_LOOP ( 'NONE', ( #575, #12834, #9761, #14902 ) ) ;
#12001=ORIENTED_EDGE ( 'NONE', *, *, #13870, .T. ) ;
#12027=LINE ( 'NONE', #17384, #14606 ) ;
#12028=EDGE_LOOP ( 'NONE', ( #8771, #4499, #10965, #7633, #17686, #14379, #9562, #17359 ) ) ;
#12036=FACE_OUTER_BOUND ( 'NONE', #15482, .T. ) ;
#12044=VECTOR ( 'NONE', #14639, 1000.000000000000000 ) ;
#12050=ORIENTED_EDGE ( 'NONE', *, *, #10606, .F. ) ;
#12053=CARTESIAN_POINT ( 'NONE',  ( -0.4000000000000000222, 2.399999999999999911, 5.100000000000000533 ) ) ;
#12059=DIRECTION ( 'NONE',  ( 1.000000000000000000, 1.233581138472399909E-16, 2.220446049250309876E-16 ) ) ;
#12062=CARTESIAN_POINT ( 'NONE',  ( 1.399999999999999911, -5.500000000000000000, 6.100000000000000533 ) ) ;
#12065=VECTOR ( 'NONE', #6439, 1000.000000000000000 ) ;
#12070=VECTOR ( 'NONE', #1277, 1000.000000000000000 ) ;
#12086=VECTOR ( 'NONE', #16862, 1000.000000000000000 ) ;
#12089=CARTESIAN_POINT ( 'NONE',  ( 6.661338147750939243E-16, 1.250000000000000000, -1.318389841742369940E-16 ) ) ;
#12106=PLANE ( 'NONE',  #16200 ) ;
#12108=CARTESIAN_POINT ( 'NONE',  ( 1.399999999999999911, 0.5999999999999999778, 3.299999999999999822 ) ) ;
#12127=LINE ( 'NONE', #5077, #9150 ) ;
#12138=CARTESIAN_POINT ( 'NONE',  ( 1.000000000000000000, -6.000000000000000000, 5.100000000000000533 ) ) ;
#12140=CARTESIAN_POINT ( 'NONE',  ( 0.5500000000000000444, -2.399999999999999911, 3.600000000000000089 ) ) ;
#12158=VECTOR ( 'NONE', #7272, 1000.000000000000000 ) ;
#12179=CARTESIAN_POINT ( 'NONE',  ( 0.5500000000000000444, 2.050000000000000266, 3.600000000000000089 ) ) ;
#12183=CARTESIAN_POINT ( 'NONE',  ( 6.735557395310439065E-16, -5.500000000000000000, -3.367778697655220026E-16 ) ) ;
#12185=CARTESIAN_POINT ( 'NONE',  ( -1.399999999999999911, -8.000000000000000000, 6.100000000000000533 ) ) ;
#12192=ORIENTED_EDGE ( 'NONE', *, *, #13109, .T. ) ;
#12196=CARTESIAN_POINT ( 'NONE',  ( 1.399999999999999911, -8.000000000000000000, 6.100000000000000533 ) ) ;
#12208=ORIENTED_EDGE ( 'NONE', *, *, #14645, .T. ) ;
#12212=EDGE_CURVE ( 'NONE', #8376, #11415, #7394, .T. ) ;
#12215=CARTESIAN_POINT ( 'NONE',  ( 1.828929293328490072E-16, 2.399999999999999911, 5.100000000000000533 ) ) ;
#12231=DIRECTION ( 'NONE',  ( -1.899065700016719806E-16, -1.000000000000000000, 0.000000000000000000 ) ) ;
#12240=ORIENTED_EDGE ( 'NONE', *, *, #9955, .T. ) ;
#12272=LINE ( 'NONE', #6526, #11701 ) ;
#12281=EDGE_LOOP ( 'NONE', ( #4029, #2818, #1865 ) ) ;
#12285=FACE_OUTER_BOUND ( 'NONE', #374, .T. ) ;
#12286=ORIENTED_EDGE ( 'NONE', *, *, #4348, .F. ) ;
#12298=PLANE ( 'NONE',  #16517 ) ;
#12303=VERTEX_POINT ( 'NONE', #8038 ) ;
#12311=ORIENTED_EDGE ( 'NONE', *, *, #2939, .T. ) ;
#12318=EDGE_CURVE ( 'NONE', #8531, #13986, #5056, .T. ) ;
#12333=ORIENTED_EDGE ( 'NONE', *, *, #15264, .F. ) ;
#12343=VECTOR ( 'NONE', #2838, 1000.000000000000000 ) ;
#12348=VECTOR ( 'NONE', #2542, 1000.000000000000000 ) ;
#12368=ORIENTED_EDGE ( 'NONE', *, *, #14430, .T. ) ;
#12369=CARTESIAN_POINT ( 'NONE',  ( 7.233457020361919865E-16, 4.000000000000000000, 5.100000000000000533 ) ) ;
#12370=CARTESIAN_POINT ( 'NONE',  ( 1.000000000000000000, -7.000000000000000000, 3.700000000000000178 ) ) ;
#12376=VERTEX_POINT ( 'NONE', #16353 ) ;
#12393=LINE ( 'NONE', #18290, #5578 ) ;
#12405=ORIENTED_EDGE ( 'NONE', *, *, #2230, .T. ) ;
#12419=LINE ( 'NONE', #8258, #15504 ) ;
#12421=ORIENTED_EDGE ( 'NONE', *, *, #7928, .T. ) ;
#12422=EDGE_CURVE ( 'NONE', #2694, #16856, #3657, .T. ) ;
#12423=VECTOR ( 'NONE', #12590, 1000.000000000000000 ) ;
#12426=VERTEX_POINT ( 'NONE', #902 ) ;
#12427=CARTESIAN_POINT ( 'NONE',  ( -0.9000000000000000222, 2.050000000000000266, 1.600000000000000089 ) ) ;
#12431=DIRECTION ( 'NONE',  ( 0.000000000000000000, -1.000000000000000000, 0.000000000000000000 ) ) ;
#12436=EDGE_CURVE ( 'NONE', #1832, #13096, #18000, .T. ) ;
#12437=PLANE ( 'NONE',  #8794 ) ;
#12441=LINE ( 'NONE', #16785, #957 ) ;
#12446=AXIS2_PLACEMENT_3D ( 'NONE', #13856, #11354, #16905 ) ;
#12454=CARTESIAN_POINT ( 'NONE',  ( -1.000000000000000000, -5.500000000000000000, 5.100000000000000533 ) ) ;
#12455=CARTESIAN_POINT ( 'NONE',  ( -1.399999999999999911, -7.000000000000000000, 6.100000000000000533 ) ) ;
#12475=DIRECTION ( 'NONE',  ( -2.854859206178970228E-16, -1.000000000000000000, 0.000000000000000000 ) ) ;
#12491=VECTOR ( 'NONE', #8338, 1000.000000000000000 ) ;
#12498=CARTESIAN_POINT ( 'NONE',  ( -0.5500000000000000444, -2.399999999999999911, 3.600000000000000089 ) ) ;
#12503=DIRECTION ( 'NONE',  ( 1.000000000000000000, -2.220446049250310320E-15, 0.000000000000000000 ) ) ;
#12506=VECTOR ( 'NONE', #7979, 1000.000000000000000 ) ;
#12510=ADVANCED_FACE ( 'NONE', ( #2555 ), #15352, .F. ) ;
#12512=ORIENTED_EDGE ( 'NONE', *, *, #17102, .F. ) ;
#12515=DIRECTION ( 'NONE',  ( -1.000000000000000000, -8.881784197001258979E-17, -1.776356839400249824E-16 ) ) ;
#12519=ADVANCED_FACE ( 'NONE', ( #18274 ), #1348, .T. ) ;
#12543=VECTOR ( 'NONE', #17279, 1000.000000000000000 ) ;
#12544=EDGE_CURVE ( 'NONE', #8588, #12303, #14395, .T. ) ;
#12563=LINE ( 'NONE', #8403, #9072 ) ;
#12571=DIRECTION ( 'NONE',  ( 1.110223024625159992E-16, 0.000000000000000000, 1.000000000000000000 ) ) ;
#12574=VERTEX_POINT ( 'NONE', #416 ) ;
#12590=DIRECTION ( 'NONE',  ( 1.110223024625159992E-16, 0.000000000000000000, 1.000000000000000000 ) ) ;
#12591=ORIENTED_EDGE ( 'NONE', *, *, #8017, .T. ) ;
#12603=CARTESIAN_POINT ( 'NONE',  ( -0.9000000000000000222, 6.450000000000000178, 3.600000000000000089 ) ) ;
#12607=VECTOR ( 'NONE', #6608, 1000.000000000000000 ) ;
#12608=DIRECTION ( 'NONE',  ( -3.392348130799090196E-16, 1.000000000000000000, 0.000000000000000000 ) ) ;
#12623=AXIS2_PLACEMENT_3D ( 'NONE', #14904, #8968, #14703 ) ;
#12656=VECTOR ( 'NONE', #9772, 1000.000000000000000 ) ;
#12679=AXIS2_PLACEMENT_3D ( 'NONE', #6847, #2500, #15191 ) ;
#12687=DIRECTION ( 'NONE',  ( 0.000000000000000000, 0.000000000000000000, -1.000000000000000000 ) ) ;
#12690=CARTESIAN_POINT ( 'NONE',  ( -0.9000000000000000222, -9.500000000000000000, 6.100000000000000533 ) ) ;
#12695=ORIENTED_EDGE ( 'NONE', *, *, #5458, .F. ) ;
#12696=LINE ( 'NONE', #6859, #14757 ) ;
#12702=PLANE ( 'NONE',  #3496 ) ;
#12709=CARTESIAN_POINT ( 'NONE',  ( 1.399999999999999911, -8.000000000000000000, 3.299999999999999822 ) ) ;
#12718=VECTOR ( 'NONE', #1097, 1000.000000000000000 ) ;
#12729=ORIENTED_EDGE ( 'NONE', *, *, #10487, .F. ) ;
#12736=CARTESIAN_POINT ( 'NONE',  ( 0.4000000000000000222, 2.399999999999999911, 5.100000000000000533 ) ) ;
#12743=VERTEX_POINT ( 'NONE', #7992 ) ;
#12770=LINE ( 'NONE', #4235, #13849 ) ;
#12780=DIRECTION ( 'NONE',  ( 1.301042606982604138E-15, -1.000000000000000000, 0.000000000000000000 ) ) ;
#12782=EDGE_CURVE ( 'NONE', #13986, #5262, #10667, .T. ) ;
#12785=CARTESIAN_POINT ( 'NONE',  ( 7.069631497386979886E-16, 5.131370849898479136, 5.100000000000000533 ) ) ;
#12790=SURFACE_SIDE_STYLE ('',( #11304 ) ) ;
#12825=EDGE_LOOP ( 'NONE', ( #13695, #2284, #125 ) ) ;
#12826=DIRECTION ( 'NONE',  ( 1.746418240983389920E-16, -1.000000000000000000, 0.000000000000000000 ) ) ;
#12828=ORIENTED_EDGE ( 'NONE', *, *, #13770, .F. ) ;
#12834=ORIENTED_EDGE ( 'NONE', *, *, #9049, .F. ) ;
#12836=VECTOR ( 'NONE', #17551, 1000.000000000000000 ) ;
#12858=DIRECTION ( 'NONE',  ( 1.000000000000000000, 0.000000000000000000, 0.000000000000000000 ) ) ;
#12862=DIRECTION ( 'NONE',  ( -2.220446049250309876E-16, 0.000000000000000000, 1.000000000000000000 ) ) ;
#12864=DIRECTION ( 'NONE',  ( 0.000000000000000000, 0.000000000000000000, 1.000000000000000000 ) ) ;
#12868=CARTESIAN_POINT ( 'NONE',  ( 0.5000000000000000000, 3.500000000000000000, 5.100000000000000533 ) ) ;
#12871=CARTESIAN_POINT ( 'NONE',  ( 1.000000000000000000, -5.000000000000000000, 6.100000000000000533 ) ) ;
#12878=EDGE_CURVE ( 'NONE', #6927, #7652, #2519, .T. ) ;
#12880=LINE ( 'NONE', #5478, #4057 ) ;
#12884=CARTESIAN_POINT ( 'NONE',  ( -1.399999999999999911, -5.500000000000000000, 5.100000000000000533 ) ) ;
#12892=EDGE_LOOP ( 'NONE', ( #9865, #7250, #656, #5531 ) ) ;
#12898=ORIENTED_EDGE ( 'NONE', *, *, #15246, .T. ) ;
#12910=LINE ( 'NONE', #11696, #375 ) ;
#12922=VERTEX_POINT ( 'NONE', #5572 ) ;
#12925=AXIS2_PLACEMENT_3D ( 'NONE', #2779, #13972, #12780 ) ;
#12929=DIRECTION ( 'NONE',  ( 1.000000000000000000, 1.189524669241239855E-16, 4.716563129111599823E-33 ) ) ;
#12930=ORIENTED_EDGE ( 'NONE', *, *, #5458, .T. ) ;
#12948=DIRECTION ( 'NONE',  ( 0.000000000000000000, 0.000000000000000000, 1.000000000000000000 ) ) ;
#12949=CARTESIAN_POINT ( 'NONE',  ( -0.5500000000000000444, 2.050000000000000266, 1.600000000000000089 ) ) ;
#12958=VECTOR ( 'NONE', #8435, 1000.000000000000000 ) ;
#12976=CARTESIAN_POINT ( 'NONE',  ( 1.800000000000000044, 7.799999999999999822, 7.599999999999999645 ) ) ;
#12979=EDGE_CURVE ( 'NONE', #13315, #1371, #2704, .T. ) ;
#12984=ORIENTED_EDGE ( 'NONE', *, *, #11113, .T. ) ;
#12995=LINE ( 'NONE', #11879, #12044 ) ;
#13006=ADVANCED_FACE ( 'NONE', ( #5475 ), #2614, .F. ) ;
#13015=ORIENTED_EDGE ( 'NONE', *, *, #3281, .F. ) ;
#13018=LINE ( 'NONE', #17437, #8214 ) ;
#13045=LINE ( 'NONE', #11745, #4646 ) ;
#13051=FACE_OUTER_BOUND ( 'NONE', #14099, .T. ) ;
#13057=CARTESIAN_POINT ( 'NONE',  ( 8.782273797403119722E-16, 6.262741699796950279, 6.100000000000000533 ) ) ;
#13069=EDGE_CURVE ( 'NONE', #8102, #4320, #11115, .T. ) ;
#13083=ORIENTED_EDGE ( 'NONE', *, *, #12318, .T. ) ;
#13084=LINE ( 'NONE', #13260, #2588 ) ;
#13088=FACE_OUTER_BOUND ( 'NONE', #3255, .T. ) ;
#13089=CARTESIAN_POINT ( 'NONE',  ( 1.250000000000000000, 3.500000000000000000, 5.100000000000000533 ) ) ;
#13096=VERTEX_POINT ( 'NONE', #720 ) ;
#13109=EDGE_CURVE ( 'NONE', #12574, #9877, #10521, .T. ) ;
#13121=DIRECTION ( 'NONE',  ( 1.224646799147350002E-16, -1.000000000000000000, -6.123233995736769734E-17 ) ) ;
#13124=ORIENTED_EDGE ( 'NONE', *, *, #18114, .T. ) ;
#13127=LINE ( 'NONE', #14597, #17936 ) ;
#13129=EDGE_LOOP ( 'NONE', ( #471, #3962, #5779, #11353 ) ) ;
#13132=CARTESIAN_POINT ( 'NONE',  ( -1.000000000000000000, -8.000000000000000000, 5.700000000000000178 ) ) ;
#13134=LINE ( 'NONE', #14336, #13809 ) ;
#13136=DIRECTION ( 'NONE',  ( 0.000000000000000000, 0.000000000000000000, 1.000000000000000000 ) ) ;
#13144=DIRECTION ( 'NONE',  ( 0.000000000000000000, 0.000000000000000000, -1.000000000000000000 ) ) ;
#13160=CARTESIAN_POINT ( 'NONE',  ( 0.4000000000000000222, -1.399999999999999911, 6.100000000000000533 ) ) ;
#13165=DIRECTION ( 'NONE',  ( -0.7071067811865480168, -0.7071067811865470176, 0.000000000000000000 ) ) ;
#13174=CARTESIAN_POINT ( 'NONE',  ( 1.800000000000000044, 0.5999999999999999778, 1.600000000000000089 ) ) ;
#13178=CARTESIAN_POINT ( 'NONE',  ( 1.399999999999999911, -5.000000000000000000, 6.100000000000000533 ) ) ;
#13181=VECTOR ( 'NONE', #2425, 1000.000000000000000 ) ;
#13195=ADVANCED_FACE ( 'NONE', ( #3675 ), #12298, .T. ) ;
#13209=AXIS2_PLACEMENT_3D ( 'NONE', #3690, #17659, #4997 ) ;
#13210=VECTOR ( 'NONE', #10261, 1000.000000000000000 ) ;
#13216=ADVANCED_FACE ( 'NONE', ( #9322 ), #2307, .T. ) ;
#13224=EDGE_CURVE ( 'NONE', #9615, #13769, #9606, .T. ) ;
#13228=VERTEX_POINT ( 'NONE', #1093 ) ;
#13232=VECTOR ( 'NONE', #12515, 1000.000000000000000 ) ;
#13240=EDGE_CURVE ( 'NONE', #16121, #14329, #12393, .T. ) ;
#13248=ORIENTED_EDGE ( 'NONE', *, *, #5414, .T. ) ;
#13253=ORIENTED_EDGE ( 'NONE', *, *, #13770, .T. ) ;
#13255=ORIENTED_EDGE ( 'NONE', *, *, #13069, .T. ) ;
#13260=CARTESIAN_POINT ( 'NONE',  ( 1.000000000000000000, -7.000000000000000000, 5.700000000000000178 ) ) ;
#13299=CARTESIAN_POINT ( 'NONE',  ( 1.399999999999999911, -8.000000000000000000, 6.100000000000000533 ) ) ;
#13315=VERTEX_POINT ( 'NONE', #1187 ) ;
#13320=VECTOR ( 'NONE', #11548, 1000.000000000000000 ) ;
#13322=EDGE_CURVE ( 'NONE', #786, #6313, #11084, .T. ) ;
#13350=EDGE_CURVE ( 'NONE', #17115, #4659, #8761, .T. ) ;
#13359=ADVANCED_FACE ( 'NONE', ( #5897, #8857 ), #17173, .T. ) ;
#13363=AXIS2_PLACEMENT_3D ( 'NONE', #1113, #13789, #7041 ) ;
#13405=CARTESIAN_POINT ( 'NONE',  ( -1.000000000000000000, -7.000000000000000000, 5.700000000000000178 ) ) ;
#13421=VECTOR ( 'NONE', #11482, 1000.000000000000000 ) ;
#13426=EDGE_CURVE ( 'NONE', #16693, #16922, #10072, .T. ) ;
#13431=EDGE_CURVE ( 'NONE', #12376, #3539, #17349, .T. ) ;
#13432=CARTESIAN_POINT ( 'NONE',  ( 0.9000000000000000222, 6.450000000000000178, 1.600000000000000089 ) ) ;
#13444=FACE_OUTER_BOUND ( 'NONE', #15074, .T. ) ;
#13484=ORIENTED_EDGE ( 'NONE', *, *, #12436, .F. ) ;
#13500=EDGE_CURVE ( 'NONE', #305, #5195, #15994, .T. ) ;
#13508=VECTOR ( 'NONE', #9859, 1000.000000000000000 ) ;
#13509=LINE ( 'NONE', #1850, #7526 ) ;
#13510=CARTESIAN_POINT ( 'NONE',  ( 1.000000000000000000, -5.000000000000000000, 3.299999999999999822 ) ) ;
#13521=CIRCLE ( 'NONE', #13209, 0.4000000000000000222 ) ;
#13529=VECTOR ( 'NONE', #7446, 1000.000000000000000 ) ;
#13533=ORIENTED_EDGE ( 'NONE', *, *, #7336, .F. ) ;
#13535=ORIENTED_EDGE ( 'NONE', *, *, #11077, .T. ) ;
#13549=ORIENTED_EDGE ( 'NONE', *, *, #16891, .T. ) ;
#13560=EDGE_LOOP ( 'NONE', ( #5966, #4056, #13248, #14105 ) ) ;
#13561=VECTOR ( 'NONE', #7882, 1000.000000000000000 ) ;
#13571=AXIS2_PLACEMENT_3D ( 'NONE', #17061, #7264, #1707 ) ;
#13585=ORIENTED_EDGE ( 'NONE', *, *, #12212, .T. ) ;
#13600=CARTESIAN_POINT ( 'NONE',  ( 0.4000000000000000222, 2.399999999999999911, 5.100000000000000533 ) ) ;
#13603=VECTOR ( 'NONE', #9235, 1000.000000000000000 ) ;
#13604=DIRECTION ( 'NONE',  ( -1.000000000000000000, -2.220446049250309876E-16, 7.930164461608259947E-17 ) ) ;
#13605=CARTESIAN_POINT ( 'NONE',  ( -5.045174592681759329E-16, -1.399999999999999911, 5.100000000000000533 ) ) ;
#13613=VERTEX_POINT ( 'NONE', #4852 ) ;
#13617=EDGE_CURVE ( 'NONE', #3744, #1832, #788, .T. ) ;
#13621=DIRECTION ( 'NONE',  ( -1.000000000000000000, 0.000000000000000000, -1.776356839400249824E-16 ) ) ;
#13630=ORIENTED_EDGE ( 'NONE', *, *, #13617, .F. ) ;
#13645=CARTESIAN_POINT ( 'NONE',  ( -0.9000000000000000222, -10.00000000000000000, 6.100000000000000533 ) ) ;
#13665=VERTEX_POINT ( 'NONE', #17326 ) ;
#13671=EDGE_LOOP ( 'NONE', ( #5344, #4984, #5789, #11932 ) ) ;
#13676=EDGE_CURVE ( 'NONE', #17390, #11415, #4657, .T. ) ;
#13695=ORIENTED_EDGE ( 'NONE', *, *, #11591, .F. ) ;
#13700=FACE_OUTER_BOUND ( 'NONE', #4077, .T. ) ;
#13718=ADVANCED_FACE ( 'NONE', ( #14569 ), #238, .F. ) ;
#13727=LINE ( 'NONE', #1137, #4033 ) ;
#13734=VECTOR ( 'NONE', #1927, 1000.000000000000000 ) ;
#13750=DIRECTION ( 'NONE',  ( 1.110223024625159992E-16, 0.000000000000000000, 1.000000000000000000 ) ) ;
#13760=ORIENTED_EDGE ( 'NONE', *, *, #1836, .F. ) ;
#13766=EDGE_CURVE ( 'NONE', #138, #4659, #7530, .T. ) ;
#13769=VERTEX_POINT ( 'NONE', #13174 ) ;
#13770=EDGE_CURVE ( 'NONE', #4320, #6296, #491, .T. ) ;
#13772=DIRECTION ( 'NONE',  ( 2.220446049250309876E-16, 5.551115123125779621E-17, -1.000000000000000000 ) ) ;
#13780=CARTESIAN_POINT ( 'NONE',  ( -3.399999999999999911, -9.500000000000000000, 3.799999999999999822 ) ) ;
#13788=CARTESIAN_POINT ( 'NONE',  ( -1.399999999999999911, 0.5999999999999999778, 3.299999999999999822 ) ) ;
#13789=DIRECTION ( 'NONE',  ( 0.000000000000000000, 0.000000000000000000, -1.000000000000000000 ) ) ;
#13798=DIRECTION ( 'NONE',  ( 1.000000000000000000, -1.899065700016719806E-16, 0.000000000000000000 ) ) ;
#13809=VECTOR ( 'NONE', #17189, 1000.000000000000000 ) ;
#13825=VECTOR ( 'NONE', #2266, 1000.000000000000000 ) ;
#13836=DIRECTION ( 'NONE',  ( 1.000000000000000000, 0.000000000000000000, 0.000000000000000000 ) ) ;
#13849=VECTOR ( 'NONE', #11462, 1000.000000000000000 ) ;
#13856=CARTESIAN_POINT ( 'NONE',  ( 1.399999999999999911, -5.500000000000000000, 5.100000000000000533 ) ) ;
#13867=PLANE ( 'NONE',  #14092 ) ;
#13870=EDGE_CURVE ( 'NONE', #7652, #5300, #16768, .T. ) ;
#13873=VECTOR ( 'NONE', #10511, 1000.000000000000000 ) ;
#13879=ORIENTED_EDGE ( 'NONE', *, *, #13224, .F. ) ;
#13882=DIRECTION ( 'NONE',  ( 1.000000000000000000, 0.000000000000000000, 0.000000000000000000 ) ) ;
#13886=CARTESIAN_POINT ( 'NONE',  ( -0.9000000000000000222, 2.050000000000000266, 3.600000000000000089 ) ) ;
#13889=DIRECTION ( 'NONE',  ( -1.746418240983389920E-16, 1.000000000000000000, 0.000000000000000000 ) ) ;
#13895=DIRECTION ( 'NONE',  ( -2.220446049250309876E-16, -5.551115123125779621E-17, 1.000000000000000000 ) ) ;
#13910=FACE_OUTER_BOUND ( 'NONE', #9146, .T. ) ;
#13933=LINE ( 'NONE', #231, #4202 ) ;
#13937=EDGE_LOOP ( 'NONE', ( #16673, #2320, #14628, #12512 ) ) ;
#13938=FACE_OUTER_BOUND ( 'NONE', #15341, .T. ) ;
#13953=CARTESIAN_POINT ( 'NONE',  ( 6.502734858518770642E-16, 3.500000000000000000, 6.100000000000000533 ) ) ;
#13960=CARTESIAN_POINT ( 'NONE',  ( -1.000000000000000000, -5.000000000000000000, 3.299999999999999822 ) ) ;
#13961=DIRECTION ( 'NONE',  ( 1.110223024625159992E-16, 0.000000000000000000, -1.000000000000000000 ) ) ;
#13963=ORIENTED_EDGE ( 'NONE', *, *, #15506, .T. ) ;
#13972=DIRECTION ( 'NONE',  ( 0.000000000000000000, 0.000000000000000000, -1.000000000000000000 ) ) ;
#13974=CARTESIAN_POINT ( 'NONE',  ( 0.5500000000000000444, 0.5999999999999999778, 3.299999999999999822 ) ) ;
#13986=VERTEX_POINT ( 'NONE', #12709 ) ;
#13987=CARTESIAN_POINT ( 'NONE',  ( 0.5500000000000000444, 2.050000000000000266, 3.600000000000000089 ) ) ;
#13991=CARTESIAN_POINT ( 'NONE',  ( 1.250000000000000000, 0.5999999999999999778, 7.599999999999999645 ) ) ;
#14005=DIRECTION ( 'NONE',  ( 2.467162276944790449E-16, 0.000000000000000000, 1.000000000000000000 ) ) ;
#14039=CARTESIAN_POINT ( 'NONE',  ( -1.250000000000000000, 7.799999999999999822, 5.100000000000000533 ) ) ;
#14052=LINE ( 'NONE', #7990, #15658 ) ;
#14058=DIRECTION ( 'NONE',  ( -6.167905692361979821E-17, 0.000000000000000000, -1.000000000000000000 ) ) ;
#14065=ORIENTED_EDGE ( 'NONE', *, *, #4843, .F. ) ;
#14068=PRESENTATION_STYLE_ASSIGNMENT (( #15835 ) ) ;
#14071=CARTESIAN_POINT ( 'NONE',  ( -1.399999999999999911, -8.000000000000000000, 3.299999999999999822 ) ) ;
#14074=CARTESIAN_POINT ( 'NONE',  ( -0.9000000000000000222, 6.450000000000000178, 3.600000000000000089 ) ) ;
#14076=DIRECTION ( 'NONE',  ( 2.490091241227950223E-32, -1.233581138472399909E-16, 1.000000000000000000 ) ) ;
#14078=VECTOR ( 'NONE', #5222, 1000.000000000000000 ) ;
#14091=VECTOR ( 'NONE', #4261, 1000.000000000000000 ) ;
#14092=AXIS2_PLACEMENT_3D ( 'NONE', #18285, #14662, #11537 ) ;
#14097=VECTOR ( 'NONE', #3560, 1000.000000000000000 ) ;
#14099=EDGE_LOOP ( 'NONE', ( #11439, #6649, #15573, #6555 ) ) ;
#14105=ORIENTED_EDGE ( 'NONE', *, *, #3843, .T. ) ;
#14119=AXIS2_PLACEMENT_3D ( 'NONE', #6041, #13165, #11793 ) ;
#14123=AXIS2_PLACEMENT_3D ( 'NONE', #11883, #10568, #14842 ) ;
#14129=ADVANCED_FACE ( 'NONE', ( #17841 ), #14815, .T. ) ;
#14135=EDGE_CURVE ( 'NONE', #2147, #17934, #13521, .T. ) ;
#14142=ORIENTED_EDGE ( 'NONE', *, *, #13240, .T. ) ;
#14143=VECTOR ( 'NONE', #17397, 1000.000000000000000 ) ;
#14152=ORIENTED_EDGE ( 'NONE', *, *, #6641, .F. ) ;
#14157=VECTOR ( 'NONE', #13144, 1000.000000000000000 ) ;
#14159=ADVANCED_FACE ( 'NONE', ( #2324 ), #17938, .T. ) ;
#14160=ORIENTED_EDGE ( 'NONE', *, *, #12878, .F. ) ;
#14167=CARTESIAN_POINT ( 'NONE',  ( 1.250000000000000000, 6.144112549695430303, 5.100000000000000533 ) ) ;
#14172=PLANE ( 'NONE',  #9698 ) ;
#14185=VECTOR ( 'NONE', #52, 1000.000000000000000 ) ;
#14192=LINE ( 'NONE', #17292, #4981 ) ;
#14196=FACE_OUTER_BOUND ( 'NONE', #13937, .T. ) ;
#14197=CARTESIAN_POINT ( 'NONE',  ( -1.800000000000000044, 7.799999999999999822, 1.600000000000000089 ) ) ;
#14202=DIRECTION ( 'NONE',  ( 0.000000000000000000, 0.000000000000000000, -1.000000000000000000 ) ) ;
#14203=VERTEX_POINT ( 'NONE', #8244 ) ;
#14209=VECTOR ( 'NONE', #7738, 1000.000000000000000 ) ;
#14217=ORIENTED_EDGE ( 'NONE', *, *, #11893, .T. ) ;
#14222=VECTOR ( 'NONE', #17006, 1000.000000000000000 ) ;
#14225=CARTESIAN_POINT ( 'NONE',  ( 0.5500000000000000444, 7.799999999999999822, 3.600000000000000089 ) ) ;
#14236=EDGE_CURVE ( 'NONE', #11589, #6491, #7484, .T. ) ;
#14241=LINE ( 'NONE', #5806, #6889 ) ;
#14246=ORIENTED_EDGE ( 'NONE', *, *, #17482, .F. ) ;
#14253=CARTESIAN_POINT ( 'NONE',  ( 5.709718412357949331E-16, 4.000000000000000000, 6.100000000000000533 ) ) ;
#14263=DIRECTION ( 'NONE',  ( 0.000000000000000000, 0.000000000000000000, 1.000000000000000000 ) ) ;
#14267=LINE ( 'NONE', #16943, #12958 ) ;
#14276=LINE ( 'NONE', #12884, #9724 ) ;
#14277=EDGE_CURVE ( 'NONE', #10849, #9615, #15819, .T. ) ;
#14281=EDGE_CURVE ( 'NONE', #490, #5888, #10245, .T. ) ;
#14285=LINE ( 'NONE', #1605, #17407 ) ;
#14298=CARTESIAN_POINT ( 'NONE',  ( 1.250000000000000000, 6.144112549695419645, 6.100000000000000533 ) ) ;
#14303=CARTESIAN_POINT ( 'NONE',  ( -1.250000000000000000, 3.500000000000000000, 6.100000000000000533 ) ) ;
#14306=ORIENTED_EDGE ( 'NONE', *, *, #18287, .F. ) ;
#14307=CARTESIAN_POINT ( 'NONE',  ( 0.5500000000000000444, 0.5999999999999999778, 3.299999999999999822 ) ) ;
#14311=ORIENTED_EDGE ( 'NONE', *, *, #5359, .T. ) ;
#14322=CARTESIAN_POINT ( 'NONE',  ( -1.399999999999999911, -7.000000000000000000, 3.299999999999999822 ) ) ;
#14326=ORIENTED_EDGE ( 'NONE', *, *, #9253, .T. ) ;
#14329=VERTEX_POINT ( 'NONE', #13132 ) ;
#14336=CARTESIAN_POINT ( 'NONE',  ( -0.5500000000000000444, 7.799999999999999822, 1.600000000000000089 ) ) ;
#14350=ADVANCED_FACE ( 'NONE', ( #15740 ), #14602, .T. ) ;
#14369=ORIENTED_EDGE ( 'NONE', *, *, #11843, .F. ) ;
#14375=ORIENTED_EDGE ( 'NONE', *, *, #10065, .F. ) ;
#14379=ORIENTED_EDGE ( 'NONE', *, *, #13322, .T. ) ;
#14387=AXIS2_PLACEMENT_3D ( 'NONE', #11017, #14642, #5283 ) ;
#14390=VERTEX_POINT ( 'NONE', #12949 ) ;
#14395=LINE ( 'NONE', #14574, #9176 ) ;
#14430=EDGE_CURVE ( 'NONE', #1528, #12922, #6634, .T. ) ;
#14431=CARTESIAN_POINT ( 'NONE',  ( 0.5000000000000000000, 5.762741699796949391, 5.100000000000000533 ) ) ;
#14435=FACE_OUTER_BOUND ( 'NONE', #9431, .T. ) ;
#14447=VERTEX_POINT ( 'NONE', #2400 ) ;
#14469=ORIENTED_EDGE ( 'NONE', *, *, #15724, .T. ) ;
#14471=ORIENTED_EDGE ( 'NONE', *, *, #3866, .T. ) ;
#14474=VERTEX_POINT ( 'NONE', #713 ) ;
#14481=ORIENTED_EDGE ( 'NONE', *, *, #10271, .T. ) ;
#14487=DIRECTION ( 'NONE',  ( -1.000000000000000000, 0.000000000000000000, 0.000000000000000000 ) ) ;
#14489=ORIENTED_EDGE ( 'NONE', *, *, #7447, .F. ) ;
#14531=CARTESIAN_POINT ( 'NONE',  ( -1.399999999999999911, -8.000000000000000000, 6.100000000000000533 ) ) ;
#14536=LINE ( 'NONE', #13057, #16817 ) ;
#14540=DIRECTION ( 'NONE',  ( -1.480297366166879989E-16, -5.921189464667500234E-16, 1.000000000000000000 ) ) ;
#14549=ORIENTED_EDGE ( 'NONE', *, *, #129, .T. ) ;
#14560=ORIENTED_EDGE ( 'NONE', *, *, #13766, .F. ) ;
#14569=FACE_OUTER_BOUND ( 'NONE', #17995, .T. ) ;
#14574=CARTESIAN_POINT ( 'NONE',  ( -1.000000000000000000, -5.000000000000000000, 6.100000000000000533 ) ) ;
#14588=ORIENTED_EDGE ( 'NONE', *, *, #10639, .T. ) ;
#14591=DIRECTION ( 'NONE',  ( 0.7071067811865480168, -0.7071067811865470176, 0.000000000000000000 ) ) ;
#14596=( LENGTH_UNIT ( ) NAMED_UNIT ( * ) SI_UNIT ( .MILLI., .METRE. ) );
#14597=CARTESIAN_POINT ( 'NONE',  ( 0.9000000000000000222, 6.450000000000000178, 3.600000000000000089 ) ) ;
#14602=PLANE ( 'NONE',  #16187 ) ;
#14606=VECTOR ( 'NONE', #7857, 1000.000000000000000 ) ;
#14613=CARTESIAN_POINT ( 'NONE',  ( -1.399999999999998579, -9.792893218813446765, 3.300000000000000266 ) ) ;
#14615=DIRECTION ( 'NONE',  ( 1.000000000000000000, 0.000000000000000000, 6.344131569286600069E-16 ) ) ;
#14616=CARTESIAN_POINT ( 'NONE',  ( -0.5500000000000000444, -2.399999999999999911, 3.600000000000000089 ) ) ;
#14617=VERTEX_POINT ( 'NONE', #15540 ) ;
#14621=ADVANCED_FACE ( 'NONE', ( #4308 ), #1087, .F. ) ;
#14626=LINE ( 'NONE', #7779, #5258 ) ;
#14627=CARTESIAN_POINT ( 'NONE',  ( -0.5500000000000000444, -2.399999999999999911, 3.600000000000000089 ) ) ;
#14628=ORIENTED_EDGE ( 'NONE', *, *, #1811, .F. ) ;
#14639=DIRECTION ( 'NONE',  ( 1.608122649676639805E-16, 1.000000000000000000, 0.000000000000000000 ) ) ;
#14641=ORIENTED_EDGE ( 'NONE', *, *, #14277, .T. ) ;
#14642=DIRECTION ( 'NONE',  ( -1.000000000000000000, 0.000000000000000000, 3.965082230804129973E-17 ) ) ;
#14645=EDGE_CURVE ( 'NONE', #2413, #2147, #12563, .T. ) ;
#14662=DIRECTION ( 'NONE',  ( -1.000000000000000000, -1.233581138472399909E-16, -2.220446049250309876E-16 ) ) ;
#14666=ADVANCED_FACE ( 'NONE', ( #16820 ), #18092, .T. ) ;
#14687=CARTESIAN_POINT ( 'NONE',  ( 1.250000000000000000, 6.144112549695419645, 6.100000000000000533 ) ) ;
#14703=DIRECTION ( 'NONE',  ( 0.000000000000000000, -0.7492686492653550800, 0.6622661785325220096 ) ) ;
#14723=EDGE_CURVE ( 'NONE', #4957, #138, #11080, .T. ) ;
#14727=VERTEX_POINT ( 'NONE', #1272 ) ;
#14738=VERTEX_POINT ( 'NONE', #14039 ) ;
#14745=ORIENTED_EDGE ( 'NONE', *, *, #2128, .F. ) ;
#14749=ORIENTED_EDGE ( 'NONE', *, *, #9107, .T. ) ;
#14757=VECTOR ( 'NONE', #5744, 1000.000000000000000 ) ;
#14787=VECTOR ( 'NONE', #14591, 1000.000000000000000 ) ;
#14794=EDGE_CURVE ( 'NONE', #851, #8308, #13018, .T. ) ;
#14803=DIRECTION ( 'NONE',  ( 1.000000000000000000, 0.000000000000000000, 0.000000000000000000 ) ) ;
#14810=LINE ( 'NONE', #14616, #14157 ) ;
#14815=CYLINDRICAL_SURFACE ( 'NONE', #5543, 0.5000000000000004441 ) ;
#14817=EDGE_CURVE ( 'NONE', #14474, #4438, #11812, .T. ) ;
#14830=ORIENTED_EDGE ( 'NONE', *, *, #4348, .T. ) ;
#14831=PLANE ( 'NONE',  #8242 ) ;
#14836=CARTESIAN_POINT ( 'NONE',  ( 1.800000000000000044, 0.5999999999999999778, 7.599999999999999645 ) ) ;
#14842=DIRECTION ( 'NONE',  ( 0.000000000000000000, 6.123233995736769734E-17, -1.000000000000000000 ) ) ;
#14850=LINE ( 'NONE', #17873, #16290 ) ;
#14854=ORIENTED_EDGE ( 'NONE', *, *, #5373, .F. ) ;
#14866=LINE ( 'NONE', #12370, #4078 ) ;
#14870=ORIENTED_EDGE ( 'NONE', *, *, #2975, .T. ) ;
#14883=LINE ( 'NONE', #2197, #13873 ) ;
#14886=AXIS2_PLACEMENT_3D ( 'NONE', #11278, #15458, #8594 ) ;
#14892=ORIENTED_EDGE ( 'NONE', *, *, #2975, .F. ) ;
#14894=DIRECTION ( 'NONE',  ( 0.000000000000000000, -1.000000000000000000, -8.881784197001250351E-16 ) ) ;
#14898=CARTESIAN_POINT ( 'NONE',  ( -1.000000000000000000, -6.000000000000000000, 5.100000000000000533 ) ) ;
#14902=ORIENTED_EDGE ( 'NONE', *, *, #1573, .T. ) ;
#14904=CARTESIAN_POINT ( 'NONE',  ( -1.250000000000000000, 3.881370849898470254, 6.100000000000000533 ) ) ;
#14933=FACE_OUTER_BOUND ( 'NONE', #1145, .T. ) ;
#14986=CARTESIAN_POINT ( 'NONE',  ( 0.5500000000000000444, -2.399999999999999911, 3.299999999999999822 ) ) ;
#14995=CYLINDRICAL_SURFACE ( 'NONE', #2056, 0.5000000000000004441 ) ;
#14998=VECTOR ( 'NONE', #12862, 1000.000000000000000 ) ;
#15005=AXIS2_PLACEMENT_3D ( 'NONE', #4863, #6079, #17264 ) ;
#15009=AXIS2_PLACEMENT_3D ( 'NONE', #12089, #10694, #16337 ) ;
#15017=ORIENTED_EDGE ( 'NONE', *, *, #8695, .T. ) ;
#15035=AXIS2_PLACEMENT_3D ( 'NONE', #18206, #13798, #12231 ) ;
#15049=ORIENTED_EDGE ( 'NONE', *, *, #15830, .T. ) ;
#15058=FACE_OUTER_BOUND ( 'NONE', #12281, .T. ) ;
#15074=EDGE_LOOP ( 'NONE', ( #11371, #6969, #9807, #1212 ) ) ;
#15081=DIRECTION ( 'NONE',  ( 2.960594732333750117E-16, -1.000000000000000000, 0.000000000000000000 ) ) ;
#15083=DIRECTION ( 'NONE',  ( 1.586032892321649771E-16, -1.000000000000000000, -7.930164461608259947E-17 ) ) ;
#15093=DIRECTION ( 'NONE',  ( 1.000000000000000000, 0.000000000000000000, 0.000000000000000000 ) ) ;
#15096=VECTOR ( 'NONE', #17112, 1000.000000000000000 ) ;
#15107=ORIENTED_EDGE ( 'NONE', *, *, #2128, .T. ) ;
#15116=DIRECTION ( 'NONE',  ( -1.000000000000000000, 0.000000000000000000, 0.000000000000000000 ) ) ;
#15118=DIRECTION ( 'NONE',  ( 0.000000000000000000, 0.000000000000000000, 1.000000000000000000 ) ) ;
#15127=VECTOR ( 'NONE', #5199, 1000.000000000000000 ) ;
#15131=LINE ( 'NONE', #3992, #2297 ) ;
#15136=ORIENTED_EDGE ( 'NONE', *, *, #5074, .F. ) ;
#15142=EDGE_CURVE ( 'NONE', #7904, #10219, #10691, .T. ) ;
#15149=LINE ( 'NONE', #8190, #3424 ) ;
#15158=EDGE_LOOP ( 'NONE', ( #9590, #8899, #5505, #15331 ) ) ;
#15159=DIRECTION ( 'NONE',  ( 8.223874256482639351E-17, -1.000000000000000000, 0.000000000000000000 ) ) ;
#15167=DIRECTION ( 'NONE',  ( 0.000000000000000000, 0.000000000000000000, -1.000000000000000000 ) ) ;
#15171=EDGE_CURVE ( 'NONE', #4627, #17672, #16426, .T. ) ;
#15191=DIRECTION ( 'NONE',  ( -1.608122649676639805E-16, -1.000000000000000000, 0.000000000000000000 ) ) ;
#15199=VECTOR ( 'NONE', #6379, 1000.000000000000000 ) ;
#15208=ORIENTED_EDGE ( 'NONE', *, *, #9822, .F. ) ;
#15210=EDGE_CURVE ( 'NONE', #3744, #8531, #9769, .T. ) ;
#15225=EDGE_CURVE ( 'NONE', #2681, #9321, #4110, .T. ) ;
#15231=VERTEX_POINT ( 'NONE', #5499 ) ;
#15236=CARTESIAN_POINT ( 'NONE',  ( -1.399999999999999911, -8.000000000000000000, 6.100000000000000533 ) ) ;
#15237=DIRECTION ( 'NONE',  ( -2.297013154396880191E-16, 1.000000000000000000, 0.000000000000000000 ) ) ;
#15241=LINE ( 'NONE', #7097, #12656 ) ;
#15246=EDGE_CURVE ( 'NONE', #1331, #14447, #15149, .T. ) ;
#15264=EDGE_CURVE ( 'NONE', #16165, #8415, #1434, .T. ) ;
#15270=CARTESIAN_POINT ( 'NONE',  ( -0.5500000000000000444, 0.5999999999999999778, 1.600000000000000089 ) ) ;
#15272=CARTESIAN_POINT ( 'NONE',  ( 1.000000000000000000, -5.000000000000000000, 3.299999999999999822 ) ) ;
#15278=PLANE ( 'NONE',  #12679 ) ;
#15294=CARTESIAN_POINT ( 'NONE',  ( -1.800000000000000044, 0.5999999999999999778, 1.600000000000000089 ) ) ;
#15313=CARTESIAN_POINT ( 'NONE',  ( 1.000000000000000000, -5.500000000000000000, 6.100000000000000533 ) ) ;
#15318=CARTESIAN_POINT ( 'NONE',  ( -1.399999999999999911, -5.500000000000000000, 5.100000000000000533 ) ) ;
#15319=VERTEX_POINT ( 'NONE', #8467 ) ;
#15331=ORIENTED_EDGE ( 'NONE', *, *, #16845, .T. ) ;
#15341=EDGE_LOOP ( 'NONE', ( #14065, #3752, #2278, #99 ) ) ;
#15343=DIRECTION ( 'NONE',  ( 0.000000000000000000, 6.123233995736769734E-17, -1.000000000000000000 ) ) ;
#15344=AXIS2_PLACEMENT_3D ( 'NONE', #2119, #6364, #636 ) ;
#15350=ORIENTED_EDGE ( 'NONE', *, *, #2059, .F. ) ;
#15352=PLANE ( 'NONE',  #2079 ) ;
#15357=AXIS2_PLACEMENT_3D ( 'NONE', #3109, #6067, #4678 ) ;
#15361=DIRECTION ( 'NONE',  ( 4.037174635000570090E-16, -1.000000000000000000, 4.482164234210289821E-32 ) ) ;
#15363=DIRECTION ( 'NONE',  ( 1.000000000000000000, 0.000000000000000000, 0.000000000000000000 ) ) ;
#15365=ORIENTED_EDGE ( 'NONE', *, *, #5359, .F. ) ;
#15370=CARTESIAN_POINT ( 'NONE',  ( -7.347880794884118997E-17, 0.5999999999999999778, 3.673940397442059498E-17 ) ) ;
#15372=ORIENTED_EDGE ( 'NONE', *, *, #13322, .F. ) ;
#15375=DIRECTION ( 'NONE',  ( 1.000000000000000000, 0.000000000000000000, 0.000000000000000000 ) ) ;
#15377=PRODUCT_DEFINITION_FORMATION_WITH_SPECIFIED_SOURCE ( 'ANY', '', #1066, .NOT_KNOWN. ) ;
#15385=AXIS2_PLACEMENT_3D ( 'NONE', #9666, #8384, #9948 ) ;
#15386=FACE_OUTER_BOUND ( 'NONE', #12028, .T. ) ;
#15417=ORIENTED_EDGE ( 'NONE', *, *, #9140, .T. ) ;
#15420=ORIENTED_EDGE ( 'NONE', *, *, #17393, .T. ) ;
#15432=CARTESIAN_POINT ( 'NONE',  ( 1.192893218813449785, -10.00000000000000000, 3.507106781186551725 ) ) ;
#15433=PLANE ( 'NONE',  #15385 ) ;
#15443=ORIENTED_EDGE ( 'NONE', *, *, #3722, .T. ) ;
#15458=DIRECTION ( 'NONE',  ( 1.224646799147350002E-16, -1.000000000000000000, -6.123233995736769734E-17 ) ) ;
#15468=VECTOR ( 'NONE', #5963, 1000.000000000000000 ) ;
#15481=ADVANCED_FACE ( 'NONE', ( #13088 ), #51, .F. ) ;
#15482=EDGE_LOOP ( 'NONE', ( #8970, #11531, #14152, #18249 ) ) ;
#15488=DIRECTION ( 'NONE',  ( 4.440892098500620245E-16, -1.000000000000000000, 0.000000000000000000 ) ) ;
#15490=DIRECTION ( 'NONE',  ( -1.531342102931250010E-16, 1.000000000000000000, 0.000000000000000000 ) ) ;
#15496=ORIENTED_EDGE ( 'NONE', *, *, #14723, .F. ) ;
#15504=VECTOR ( 'NONE', #18121, 999.9999999999998863 ) ;
#15506=EDGE_CURVE ( 'NONE', #2878, #2905, #7181, .T. ) ;
#15513=ORIENTED_EDGE ( 'NONE', *, *, #10583, .F. ) ;
#15519=CARTESIAN_POINT ( 'NONE',  ( 0.5500000000000000444, 7.799999999999999822, 3.600000000000000089 ) ) ;
#15520=MECHANICAL_DESIGN_GEOMETRIC_PRESENTATION_REPRESENTATION('',(#8692),#3362);
#15528=ADVANCED_FACE ( 'NONE', ( #3274 ), #133, .T. ) ;
#15532=ORIENTED_EDGE ( 'NONE', *, *, #3937, .F. ) ;
#15536=ORIENTED_EDGE ( 'NONE', *, *, #11591, .T. ) ;
#15540=CARTESIAN_POINT ( 'NONE',  ( 0.5500000000000000444, -2.399999999999999911, 3.600000000000000089 ) ) ;
#15542=CARTESIAN_POINT ( 'NONE',  ( 1.250000000000000000, 0.5999999999999999778, 6.100000000000000533 ) ) ;
#15543=ORIENTED_EDGE ( 'NONE', *, *, #16987, .F. ) ;
#15550=ORIENTED_EDGE ( 'NONE', *, *, #881, .T. ) ;
#15565=ORIENTED_EDGE ( 'NONE', *, *, #1894, .T. ) ;
#15567=VERTEX_POINT ( 'NONE', #4821 ) ;
#15569=( NAMED_UNIT ( * ) SI_UNIT ( $, .STERADIAN. ) SOLID_ANGLE_UNIT ( ) );
#15570=ORIENTED_EDGE ( 'NONE', *, *, #1236, .F. ) ;
#15573=ORIENTED_EDGE ( 'NONE', *, *, #15735, .T. ) ;
#15581=VECTOR ( 'NONE', #4648, 1000.000000000000000 ) ;
#15583=CARTESIAN_POINT ( 'NONE',  ( 1.399999999999999911, -8.000000000000000000, 3.299999999999999822 ) ) ;
#15611=CARTESIAN_POINT ( 'NONE',  ( 1.000000000000000000, -5.500000000000000000, 5.100000000000000533 ) ) ;
#15612=EDGE_CURVE ( 'NONE', #6456, #16165, #16052, .T. ) ;
#15616=VECTOR ( 'NONE', #5875, 1000.000000000000000 ) ;
#15617=ORIENTED_EDGE ( 'NONE', *, *, #13109, .F. ) ;
#15624=LINE ( 'NONE', #1344, #10955 ) ;
#15634=DIRECTION ( 'NONE',  ( -1.000000000000000000, 0.000000000000000000, 0.000000000000000000 ) ) ;
#15643=CIRCLE ( 'NONE', #3487, 0.4000000000000000222 ) ;
#15644=DIRECTION ( 'NONE',  ( -1.000000000000000000, 0.000000000000000000, 0.000000000000000000 ) ) ;
#15647=CARTESIAN_POINT ( 'NONE',  ( -0.4058874503045720172, 7.799999999999999822, 5.100000000000000533 ) ) ;
#15652=LINE ( 'NONE', #8416, #14222 ) ;
#15658=VECTOR ( 'NONE', #15375, 1000.000000000000000 ) ;
#15667=DIRECTION ( 'NONE',  ( 1.000000000000000000, 2.220446049250309876E-16, -7.930164461608259947E-17 ) ) ;
#15686=CIRCLE ( 'NONE', #10057, 0.4000000000000000222 ) ;
#15700=CARTESIAN_POINT ( 'NONE',  ( 1.399999999999999911, -9.500000000000000000, 3.299999999999999822 ) ) ;
#15716=ORIENTED_EDGE ( 'NONE', *, *, #15612, .T. ) ;
#15724=EDGE_CURVE ( 'NONE', #9388, #490, #9360, .T. ) ;
#15725=DIRECTION ( 'NONE',  ( 1.000000000000000000, -2.220446049250310320E-15, 0.000000000000000000 ) ) ;
#15735=EDGE_CURVE ( 'NONE', #3530, #5195, #8517, .T. ) ;
#15736=DIRECTION ( 'NONE',  ( -1.233581138472399909E-16, 1.000000000000000000, 1.233581138472399909E-16 ) ) ;
#15739=CARTESIAN_POINT ( 'NONE',  ( 1.399999999999999911, 0.5999999999999999778, 6.100000000000000533 ) ) ;
#15740=FACE_OUTER_BOUND ( 'NONE', #11674, .T. ) ;
#15751=DIRECTION ( 'NONE',  ( 0.000000000000000000, 0.000000000000000000, -1.000000000000000000 ) ) ;
#15752=ORIENTED_EDGE ( 'NONE', *, *, #436, .T. ) ;
#15758=LINE ( 'NONE', #3066, #4665 ) ;
#15789=EDGE_LOOP ( 'NONE', ( #4775, #6099, #13124, #15417 ) ) ;
#15790=CARTESIAN_POINT ( 'NONE',  ( 1.399999999999999911, 0.5999999999999999778, 6.100000000000000533 ) ) ;
#15799=FACE_OUTER_BOUND ( 'NONE', #11302, .T. ) ;
#15809=VERTEX_POINT ( 'NONE', #18113 ) ;
#15818=CARTESIAN_POINT ( 'NONE',  ( -1.250000000000000000, 5.012741699796949391, 5.100000000000000533 ) ) ;
#15819=LINE ( 'NONE', #3388, #4339 ) ;
#15822=ADVANCED_FACE ( 'NONE', ( #8612 ), #8339, .F. ) ;
#15830=EDGE_CURVE ( 'NONE', #7556, #7904, #13134, .T. ) ;
#15835=SURFACE_STYLE_USAGE ( .BOTH. , #12790 ) ;
#15846=LINE ( 'NONE', #4619, #8818 ) ;
#15858=ORIENTED_EDGE ( 'NONE', *, *, #11733, .F. ) ;
#15869=ADVANCED_FACE ( 'NONE', ( #3048 ), #4591, .F. ) ;
#15874=ORIENTED_EDGE ( 'NONE', *, *, #3688, .T. ) ;
#15875=DIRECTION ( 'NONE',  ( 0.7071067811865470176, -0.7071067811865480168, 0.000000000000000000 ) ) ;
#15882=AXIS2_PLACEMENT_3D ( 'NONE', #755, #12059, #9465 ) ;
#15885=ORIENTED_EDGE ( 'NONE', *, *, #11964, .T. ) ;
#15888=CARTESIAN_POINT ( 'NONE',  ( 0.5000000000000000000, 5.762741699796949391, 6.100000000000000533 ) ) ;
#15893=LINE ( 'NONE', #3205, #18279 ) ;
#15907=ORIENTED_EDGE ( 'NONE', *, *, #2272, .F. ) ;
#15909=PLANE ( 'NONE',  #15005 ) ;
#15920=DIRECTION ( 'NONE',  ( -1.000000000000000000, 0.000000000000000000, 2.220446049250319983E-16 ) ) ;
#15923=VECTOR ( 'NONE', #11452, 1000.000000000000000 ) ;
#15929=EDGE_LOOP ( 'NONE', ( #5726, #15716, #18193, #17784 ) ) ;
#15930=FACE_OUTER_BOUND ( 'NONE', #6389, .T. ) ;
#15934=AXIS2_PLACEMENT_3D ( 'NONE', #2814, #8556, #14202 ) ;
#15935=ORIENTED_EDGE ( 'NONE', *, *, #11843, .T. ) ;
#15954=ORIENTED_EDGE ( 'NONE', *, *, #17063, .F. ) ;
#15968=CARTESIAN_POINT ( 'NONE',  ( -1.250000000000000000, 7.799999999999999822, 5.100000000000000533 ) ) ;
#15975=ORIENTED_EDGE ( 'NONE', *, *, #3144, .F. ) ;
#15988=DIRECTION ( 'NONE',  ( 0.000000000000000000, 0.000000000000000000, 1.000000000000000000 ) ) ;
#15994=LINE ( 'NONE', #3298, #15923 ) ;
#16002=ORIENTED_EDGE ( 'NONE', *, *, #3937, .T. ) ;
#16013=DIRECTION ( 'NONE',  ( -1.480297366166879989E-16, 0.000000000000000000, 1.000000000000000000 ) ) ;
#16022=CARTESIAN_POINT ( 'NONE',  ( -1.192893218813449785, -10.00000000000000000, 3.507106781186551725 ) ) ;
#16023=ORIENTED_EDGE ( 'NONE', *, *, #6779, .F. ) ;
#16024=CARTESIAN_POINT ( 'NONE',  ( 0.5500000000000000444, 6.450000000000000178, 3.600000000000000089 ) ) ;
#16037=ORIENTED_EDGE ( 'NONE', *, *, #1455, .F. ) ;
#16047=CARTESIAN_POINT ( 'NONE',  ( -1.399999999999999911, -5.500000000000000000, 6.100000000000000533 ) ) ;
#16048=CARTESIAN_POINT ( 'NONE',  ( 1.399999999999999911, 0.5999999999999999778, 6.100000000000000533 ) ) ;
#16052=LINE ( 'NONE', #18033, #17033 ) ;
#16060=LINE ( 'NONE', #15790, #17736 ) ;
#16073=ORIENTED_EDGE ( 'NONE', *, *, #7245, .F. ) ;
#16074=CARTESIAN_POINT ( 'NONE',  ( -1.399999999999999911, -6.000000000000000000, 5.100000000000000533 ) ) ;
#16080=CARTESIAN_POINT ( 'NONE',  ( 1.000000000000000000, -8.000000000000000000, 3.700000000000000178 ) ) ;
#16106=ORIENTED_EDGE ( 'NONE', *, *, #9140, .F. ) ;
#16115=LINE ( 'NONE', #10285, #6490 ) ;
#16120=VERTEX_POINT ( 'NONE', #999 ) ;
#16121=VERTEX_POINT ( 'NONE', #17914 ) ;
#16122=LINE ( 'NONE', #11681, #13561 ) ;
#16123=ORIENTED_EDGE ( 'NONE', *, *, #1578, .T. ) ;
#16128=ADVANCED_FACE ( 'NONE', ( #5259 ), #10913, .T. ) ;
#16133=ORIENTED_EDGE ( 'NONE', *, *, #177, .T. ) ;
#16139=LINE ( 'NONE', #3440, #17098 ) ;
#16165=VERTEX_POINT ( 'NONE', #18178 ) ;
#16167=VERTEX_POINT ( 'NONE', #8221 ) ;
#16185=VECTOR ( 'NONE', #1535, 1000.000000000000000 ) ;
#16186=DIRECTION ( 'NONE',  ( 0.7071067811865474617, 0.7071067811865474617, 0.000000000000000000 ) ) ;
#16187=AXIS2_PLACEMENT_3D ( 'NONE', #5999, #1653, #16013 ) ;
#16196=AXIS2_PLACEMENT_3D ( 'NONE', #7066, #6954, #11398 ) ;
#16200=AXIS2_PLACEMENT_3D ( 'NONE', #5057, #7654, #10709 ) ;
#16202=DIRECTION ( 'NONE',  ( 1.000000000000000000, 2.018587317500279868E-16, 1.110223024625159992E-16 ) ) ;
#16207=VECTOR ( 'NONE', #15736, 1000.000000000000000 ) ;
#16210=CARTESIAN_POINT ( 'NONE',  ( -1.399999999999999911, 0.5999999999999999778, 3.299999999999999822 ) ) ;
#16233=ORIENTED_EDGE ( 'NONE', *, *, #6636, .F. ) ;
#16235=CARTESIAN_POINT ( 'NONE',  ( -1.250000000000000000, 7.799999999999999822, 7.599999999999999645 ) ) ;
#16255=VERTEX_POINT ( 'NONE', #15542 ) ;
#16256=VECTOR ( 'NONE', #14803, 1000.000000000000000 ) ;
#16257=LINE ( 'NONE', #2084, #14097 ) ;
#16265=CARTESIAN_POINT ( 'NONE',  ( -0.5500000000000000444, 2.050000000000000266, 3.600000000000000089 ) ) ;
#16278=ORIENTED_EDGE ( 'NONE', *, *, #16891, .F. ) ;
#16287=CARTESIAN_POINT ( 'NONE',  ( -0.9000000000000000222, -10.00000000000000000, 3.799999999999999822 ) ) ;
#16289=DIRECTION ( 'NONE',  ( 1.000000000000000000, 0.000000000000000000, -2.379049338482479710E-16 ) ) ;
#16290=VECTOR ( 'NONE', #2164, 1000.000000000000000 ) ;
#16291=FACE_OUTER_BOUND ( 'NONE', #10900, .T. ) ;
#16292=EDGE_LOOP ( 'NONE', ( #638, #3554, #11525, #5472 ) ) ;
#16293=ORIENTED_EDGE ( 'NONE', *, *, #16987, .T. ) ;
#16308=ORIENTED_EDGE ( 'NONE', *, *, #16840, .F. ) ;
#16309=ORIENTED_EDGE ( 'NONE', *, *, #6740, .T. ) ;
#16310=EDGE_CURVE ( 'NONE', #16755, #9388, #10998, .T. ) ;
#16311=LINE ( 'NONE', #13160, #7358 ) ;
#16316=ADVANCED_FACE ( 'NONE', ( #3952 ), #13867, .T. ) ;
#16323=ORIENTED_EDGE ( 'NONE', *, *, #9132, .T. ) ;
#16337=DIRECTION ( 'NONE',  ( -1.480297366166879989E-16, 0.000000000000000000, 1.000000000000000000 ) ) ;
#16340=EDGE_LOOP ( 'NONE', ( #5101, #8480, #15543, #16610 ) ) ;
#16342=CARTESIAN_POINT ( 'NONE',  ( -1.250000000000000000, 0.5999999999999999778, 6.100000000000000533 ) ) ;
#16353=CARTESIAN_POINT ( 'NONE',  ( -1.250000000000000000, 3.500000000000000000, 5.100000000000000533 ) ) ;
#16376=ORIENTED_EDGE ( 'NONE', *, *, #9976, .T. ) ;
#16386=DIRECTION ( 'NONE',  ( 4.336808689942013792E-16, -1.000000000000000000, 0.000000000000000000 ) ) ;
#16393=CARTESIAN_POINT ( 'NONE',  ( -1.399999999999999911, -5.000000000000000000, 3.299999999999999822 ) ) ;
#16397=CARTESIAN_POINT ( 'NONE',  ( -1.000000000000000000, -5.500000000000000000, 6.100000000000000533 ) ) ;
#16401=VERTEX_POINT ( 'NONE', #5800 ) ;
#16408=LINE ( 'NONE', #6592, #17346 ) ;
#16412=ORIENTED_EDGE ( 'NONE', *, *, #4278, .F. ) ;
#16426=LINE ( 'NONE', #3731, #12607 ) ;
#16433=DIRECTION ( 'NONE',  ( 0.000000000000000000, 1.000000000000000000, 0.000000000000000000 ) ) ;
#16458=ORIENTED_EDGE ( 'NONE', *, *, #11178, .T. ) ;
#16470=ORIENTED_EDGE ( 'NONE', *, *, #13350, .T. ) ;
#16476=DIRECTION ( 'NONE',  ( -2.018587317500279868E-16, 1.000000000000000000, 0.000000000000000000 ) ) ;
#16494=ADVANCED_FACE ( 'NONE', ( #15799 ), #4758, .T. ) ;
#16517=AXIS2_PLACEMENT_3D ( 'NONE', #9522, #8054, #14894 ) ;
#16531=LINE ( 'NONE', #9491, #3786 ) ;
#16535=LINE ( 'NONE', #10785, #856 ) ;
#16540=EDGE_CURVE ( 'NONE', #16693, #4545, #2463, .T. ) ;
#16550=PLANE ( 'NONE',  #9061 ) ;
#16570=CARTESIAN_POINT ( 'NONE',  ( -0.5500000000000000444, 6.450000000000000178, 3.600000000000000089 ) ) ;
#16585=VECTOR ( 'NONE', #7835, 1000.000000000000000 ) ;
#16591=EDGE_LOOP ( 'NONE', ( #10525, #14142, #14549, #13585 ) ) ;
#16595=ORIENTED_EDGE ( 'NONE', *, *, #17038, .F. ) ;
#16598=CARTESIAN_POINT ( 'NONE',  ( 1.250000000000000000, 3.500000000000000000, 5.100000000000000533 ) ) ;
#16610=ORIENTED_EDGE ( 'NONE', *, *, #10898, .T. ) ;
#16627=CARTESIAN_POINT ( 'NONE',  ( 1.000000000000000000, -6.000000000000000000, 3.299999999999999822 ) ) ;
#16629=CARTESIAN_POINT ( 'NONE',  ( 7.069631497386979886E-16, 5.131370849898479136, 6.100000000000000533 ) ) ;
#16630=CARTESIAN_POINT ( 'NONE',  ( 1.224646799147349904E-15, -10.00000000000000000, -6.123233995736771213E-16 ) ) ;
#16639=DIRECTION ( 'NONE',  ( -2.220446049250309876E-16, -1.480297366166879989E-16, 1.000000000000000000 ) ) ;
#16644=EDGE_CURVE ( 'NONE', #2681, #16120, #687, .T. ) ;
#16647=CARTESIAN_POINT ( 'NONE',  ( 1.399999999999999911, -9.500000000000000000, 3.299999999999999822 ) ) ;
#16650=CARTESIAN_POINT ( 'NONE',  ( 0.9000000000000000222, 2.050000000000000266, 1.600000000000000089 ) ) ;
#16655=ADVANCED_FACE ( 'NONE', ( #781 ), #6419, .F. ) ;
#16664=DIRECTION ( 'NONE',  ( -1.000000000000000000, 0.000000000000000000, 1.257750167763089819E-32 ) ) ;
#16673=ORIENTED_EDGE ( 'NONE', *, *, #18057, .F. ) ;
#16676=EDGE_LOOP ( 'NONE', ( #7697, #15208, #12311, #8997 ) ) ;
#16689=VECTOR ( 'NONE', #18020, 1000.000000000000000 ) ;
#16693=VERTEX_POINT ( 'NONE', #16627 ) ;
#16699=CARTESIAN_POINT ( 'NONE',  ( 0.5500000000000000444, 6.450000000000000178, 3.600000000000000089 ) ) ;
#16703=FACE_OUTER_BOUND ( 'NONE', #17722, .T. ) ;
#16709=DIRECTION ( 'NONE',  ( 0.000000000000000000, 2.220446049250309876E-16, -1.000000000000000000 ) ) ;
#16726=ORIENTED_EDGE ( 'NONE', *, *, #10377, .F. ) ;
#16742=ORIENTED_EDGE ( 'NONE', *, *, #9822, .T. ) ;
#16755=VERTEX_POINT ( 'NONE', #5607 ) ;
#16768=LINE ( 'NONE', #12603, #8785 ) ;
#16785=CARTESIAN_POINT ( 'NONE',  ( 1.399999999999999911, -6.000000000000000000, 3.299999999999999822 ) ) ;
#16791=VECTOR ( 'NONE', #7039, 1000.000000000000000 ) ;
#16817=VECTOR ( 'NONE', #11856, 1000.000000000000000 ) ;
#16820=FACE_OUTER_BOUND ( 'NONE', #17113, .T. ) ;
#16831=CARTESIAN_POINT ( 'NONE',  ( 1.000000000000000000, -8.000000000000000000, 5.700000000000000178 ) ) ;
#16836=DIRECTION ( 'NONE',  ( 0.000000000000000000, 0.000000000000000000, 1.000000000000000000 ) ) ;
#16840=EDGE_CURVE ( 'NONE', #6456, #11596, #15241, .T. ) ;
#16845=EDGE_CURVE ( 'NONE', #9321, #17934, #5422, .T. ) ;
#16856=VERTEX_POINT ( 'NONE', #8569 ) ;
#16862=DIRECTION ( 'NONE',  ( 2.018587317500279868E-16, -1.000000000000000000, -5.046468293750709530E-17 ) ) ;
#16883=EDGE_CURVE ( 'NONE', #16255, #10849, #11602, .T. ) ;
#16891=EDGE_CURVE ( 'NONE', #4627, #16693, #3277, .T. ) ;
#16899=DIRECTION ( 'NONE',  ( 0.000000000000000000, 6.123233995736769734E-17, -1.000000000000000000 ) ) ;
#16902=DIRECTION ( 'NONE',  ( 1.000000000000000000, 0.000000000000000000, 0.000000000000000000 ) ) ;
#16905=DIRECTION ( 'NONE',  ( -2.220446049250319983E-16, 0.000000000000000000, -1.000000000000000000 ) ) ;
#16911=DIRECTION ( 'NONE',  ( 0.000000000000000000, 0.000000000000000000, 1.000000000000000000 ) ) ;
#16922=VERTEX_POINT ( 'NONE', #10391 ) ;
#16943=CARTESIAN_POINT ( 'NONE',  ( 1.000000000000000000, -5.500000000000000000, 5.100000000000000533 ) ) ;
#16948=ADVANCED_FACE ( 'NONE', ( #1825 ), #11819, .F. ) ;
#16955=DIRECTION ( 'NONE',  ( 0.000000000000000000, -1.000000000000000000, 0.000000000000000000 ) ) ;
#16981=ORIENTED_EDGE ( 'NONE', *, *, #8793, .F. ) ;
#16982=FACE_OUTER_BOUND ( 'NONE', #17552, .T. ) ;
#16987=EDGE_CURVE ( 'NONE', #11273, #15567, #11715, .T. ) ;
#16994=DIRECTION ( 'NONE',  ( -1.110223024625159992E-16, 1.000000000000000000, 0.000000000000000000 ) ) ;
#17006=DIRECTION ( 'NONE',  ( 1.000000000000000000, -5.363760801114599979E-16, 0.000000000000000000 ) ) ;
#17009=CARTESIAN_POINT ( 'NONE',  ( -1.399999999999999911, 0.5999999999999999778, 6.100000000000000533 ) ) ;
#17013=CARTESIAN_POINT ( 'NONE',  ( 1.000000000000000000, -5.500000000000000000, 6.100000000000000533 ) ) ;
#17017=DIRECTION ( 'NONE',  ( 0.000000000000000000, 0.000000000000000000, -1.000000000000000000 ) ) ;
#17021=CARTESIAN_POINT ( 'NONE',  ( -0.5500000000000000444, -2.399999999999999911, 3.299999999999999822 ) ) ;
#17023=AXIS2_PLACEMENT_3D ( 'NONE', #978, #15920, #16433 ) ;
#17024=FILL_AREA_STYLE ('',( #11565 ) ) ;
#17027=EDGE_LOOP ( 'NONE', ( #7876, #426, #10924, #11230 ) ) ;
#17029=DIRECTION ( 'NONE',  ( 0.000000000000000000, 0.000000000000000000, 1.000000000000000000 ) ) ;
#17033=VECTOR ( 'NONE', #5183, 1000.000000000000000 ) ;
#17038=EDGE_CURVE ( 'NONE', #3716, #11589, #607, .T. ) ;
#17042=ADVANCED_FACE ( 'NONE', ( #8522 ), #14172, .F. ) ;
#17044=ORIENTED_EDGE ( 'NONE', *, *, #12782, .T. ) ;
#17061=CARTESIAN_POINT ( 'NONE',  ( -0.9000000000000000222, 2.050000000000000266, 3.600000000000000089 ) ) ;
#17063=EDGE_CURVE ( 'NONE', #17390, #13613, #14866, .T. ) ;
#17068=CARTESIAN_POINT ( 'NONE',  ( 8.549934884138839976E-16, 6.262741699796950279, 5.100000000000000533 ) ) ;
#17069=ORIENTED_EDGE ( 'NONE', *, *, #6755, .F. ) ;
#17070=AXIS2_PLACEMENT_3D ( 'NONE', #2986, #17029, #109 ) ;
#17097=CARTESIAN_POINT ( 'NONE',  ( 1.250000000000000000, 0.5999999999999999778, 7.599999999999999645 ) ) ;
#17098=VECTOR ( 'NONE', #9089, 1000.000000000000000 ) ;
#17102=EDGE_CURVE ( 'NONE', #6472, #12303, #7733, .T. ) ;
#17112=DIRECTION ( 'NONE',  ( 0.000000000000000000, -1.000000000000000000, 0.000000000000000000 ) ) ;
#17113=EDGE_LOOP ( 'NONE', ( #6469, #8379, #12192, #16742 ) ) ;
#17115=VERTEX_POINT ( 'NONE', #16342 ) ;
#17119=VECTOR ( 'NONE', #1161, 1000.000000000000000 ) ;
#17127=CARTESIAN_POINT ( 'NONE',  ( -0.4000000000000000222, 2.399999999999999911, 6.100000000000000533 ) ) ;
#17133=LINE ( 'NONE', #5767, #8858 ) ;
#17148=DIRECTION ( 'NONE',  ( 9.654113257610059070E-17, 0.000000000000000000, 1.000000000000000000 ) ) ;
#17165=CARTESIAN_POINT ( 'NONE',  ( 0.9000000000000000222, 6.450000000000000178, 3.600000000000000089 ) ) ;
#17172=ORIENTED_EDGE ( 'NONE', *, *, #10277, .T. ) ;
#17173=PLANE ( 'NONE',  #15357 ) ;
#17187=CARTESIAN_POINT ( 'NONE',  ( 0.5500000000000000444, 7.799999999999999822, 1.600000000000000089 ) ) ;
#17189=DIRECTION ( 'NONE',  ( 1.110223024625159992E-16, 0.000000000000000000, -1.000000000000000000 ) ) ;
#17198=ADVANCED_FACE ( 'NONE', ( #2830 ), #5787, .F. ) ;
#17211=VECTOR ( 'NONE', #1363, 1000.000000000000000 ) ;
#17213=DIRECTION ( 'NONE',  ( -1.233581138472399909E-16, 1.000000000000000000, 6.167905692361979821E-17 ) ) ;
#17225=VECTOR ( 'NONE', #7934, 1000.000000000000000 ) ;
#17230=PLANE ( 'NONE',  #13571 ) ;
#17250=ADVANCED_FACE ( 'NONE', ( #16982 ), #8476, .T. ) ;
#17260=FACE_OUTER_BOUND ( 'NONE', #4472, .T. ) ;
#17264=DIRECTION ( 'NONE',  ( -1.110223024625159992E-16, 0.000000000000000000, -1.000000000000000000 ) ) ;
#17271=ADVANCED_FACE ( 'NONE', ( #9775 ), #11062, .F. ) ;
#17279=DIRECTION ( 'NONE',  ( -0.7071067811865470176, -0.7071067811865480168, 0.000000000000000000 ) ) ;
#17292=CARTESIAN_POINT ( 'NONE',  ( -1.399999999999999911, -5.500000000000000000, 5.100000000000000533 ) ) ;
#17295=CIRCLE ( 'NONE', #11421, 0.5000000000000000000 ) ;
#17298=LINE ( 'NONE', #10187, #3230 ) ;
#17306=CARTESIAN_POINT ( 'NONE',  ( -4.440892098500630106E-16, -1.399999999999999911, 6.100000000000000533 ) ) ;
#17318=DIRECTION ( 'NONE',  ( -1.000000000000000000, -1.644774851296529842E-16, -1.110223024625159992E-16 ) ) ;
#17324=ORIENTED_EDGE ( 'NONE', *, *, #6543, .F. ) ;
#17326=CARTESIAN_POINT ( 'NONE',  ( -1.000000000000000000, -6.000000000000000000, 5.100000000000000533 ) ) ;
#17328=AXIS2_PLACEMENT_3D ( 'NONE', #14431, #8778, #10250 ) ;
#17346=VECTOR ( 'NONE', #8171, 1000.000000000000000 ) ;
#17347=VECTOR ( 'NONE', #3269, 1000.000000000000000 ) ;
#17349=LINE ( 'NONE', #10228, #8825 ) ;
#17357=AXIS2_PLACEMENT_3D ( 'NONE', #4117, #8301, #16899 ) ;
#17358=AXIS2_PLACEMENT_3D ( 'NONE', #8217, #6830, #16994 ) ;
#17359=ORIENTED_EDGE ( 'NONE', *, *, #5974, .T. ) ;
#17384=CARTESIAN_POINT ( 'NONE',  ( -0.5500000000000000444, 0.5999999999999999778, 1.600000000000000089 ) ) ;
#17390=VERTEX_POINT ( 'NONE', #4295 ) ;
#17393=EDGE_CURVE ( 'NONE', #8415, #14738, #17534, .T. ) ;
#17397=DIRECTION ( 'NONE',  ( 0.000000000000000000, 0.000000000000000000, 1.000000000000000000 ) ) ;
#17401=DIRECTION ( 'NONE',  ( -1.233581138472399909E-16, 1.000000000000000000, 6.167905692361979821E-17 ) ) ;
#17407=VECTOR ( 'NONE', #7339, 1000.000000000000000 ) ;
#17408=ORIENTED_EDGE ( 'NONE', *, *, #10281, .T. ) ;
#17415=CARTESIAN_POINT ( 'NONE',  ( -1.399999999999999911, -5.500000000000000000, 5.100000000000000533 ) ) ;
#17421=CARTESIAN_POINT ( 'NONE',  ( 1.000000000000000000, -5.000000000000000000, 3.299999999999999822 ) ) ;
#17437=CARTESIAN_POINT ( 'NONE',  ( 1.399999999999999911, -5.500000000000000000, 5.100000000000000533 ) ) ;
#17459=LINE ( 'NONE', #14687, #7332 ) ;
#17469=DIRECTION ( 'NONE',  ( 1.480297366166879989E-16, 7.401486830834378990E-17, -1.000000000000000000 ) ) ;
#17482=EDGE_CURVE ( 'NONE', #356, #8350, #797, .T. ) ;
#17491=ADVANCED_FACE ( 'NONE', ( #9308 ), #12106, .T. ) ;
#17499=LINE ( 'NONE', #15968, #17347 ) ;
#17509=EDGE_CURVE ( 'NONE', #5262, #9388, #9416, .T. ) ;
#17518=LINE ( 'NONE', #7217, #9244 ) ;
#17523=DIRECTION ( 'NONE',  ( 1.110223024625159992E-16, 0.000000000000000000, -1.000000000000000000 ) ) ;
#17529=DIRECTION ( 'NONE',  ( 0.000000000000000000, 0.000000000000000000, 1.000000000000000000 ) ) ;
#17534=LINE ( 'NONE', #6339, #6741 ) ;
#17535=CARTESIAN_POINT ( 'NONE',  ( 1.250000000000000000, 7.799999999999999822, 7.599999999999999645 ) ) ;
#17545=VECTOR ( 'NONE', #10750, 1000.000000000000000 ) ;
#17551=DIRECTION ( 'NONE',  ( 1.000000000000000000, 0.000000000000000000, -2.467162276944790449E-16 ) ) ;
#17552=EDGE_LOOP ( 'NONE', ( #14870, #4166, #7646, #190 ) ) ;
#17565=ORIENTED_EDGE ( 'NONE', *, *, #13426, .T. ) ;
#17577=APPLICATION_CONTEXT ( 'automotive_design' ) ;
#17585=CARTESIAN_POINT ( 'NONE',  ( 1.250000000000000000, 3.500000000000000000, 6.100000000000000533 ) ) ;
#17603=CARTESIAN_POINT ( 'NONE',  ( 0.4000000000000000222, -1.399999999999999911, 5.100000000000000533 ) ) ;
#17613=LINE ( 'NONE', #11042, #17225 ) ;
#17638=AXIS2_PLACEMENT_3D ( 'NONE', #9011, #12929, #257 ) ;
#17643=DIRECTION ( 'NONE',  ( -9.796085511398438540E-17, -8.106125845929150651E-31, -1.000000000000000000 ) ) ;
#17645=EDGE_LOOP ( 'NONE', ( #4920, #10558, #4076, #6748, #16323, #3627 ) ) ;
#17647=LINE ( 'NONE', #3593, #13734 ) ;
#17648=ORIENTED_EDGE ( 'NONE', *, *, #4872, .F. ) ;
#17659=DIRECTION ( 'NONE',  ( 0.000000000000000000, 0.000000000000000000, -1.000000000000000000 ) ) ;
#17672=VERTEX_POINT ( 'NONE', #1349 ) ;
#17676=AXIS2_PLACEMENT_3D ( 'NONE', #13987, #5301, #1305 ) ;
#17681=AXIS2_PLACEMENT_3D ( 'NONE', #11191, #16836, #4146 ) ;
#17686=ORIENTED_EDGE ( 'NONE', *, *, #111, .T. ) ;
#17691=ORIENTED_EDGE ( 'NONE', *, *, #1266, .F. ) ;
#17692=CARTESIAN_POINT ( 'NONE',  ( 7.771561172376099727E-16, 5.131370849898479136, 5.100000000000000533 ) ) ;
#17693=CYLINDRICAL_SURFACE ( 'NONE', #7954, 0.4000000000000000222 ) ;
#17700=CARTESIAN_POINT ( 'NONE',  ( 1.399999999999999911, -5.000000000000000000, 3.299999999999999822 ) ) ;
#17717=VECTOR ( 'NONE', #3960, 1000.000000000000000 ) ;
#17722=EDGE_LOOP ( 'NONE', ( #42, #3963, #3279, #4123 ) ) ;
#17727=CARTESIAN_POINT ( 'NONE',  ( 1.399999999999999911, -5.000000000000000000, 3.299999999999999822 ) ) ;
#17734=DIRECTION ( 'NONE',  ( -1.340940200278649995E-16, 1.000000000000000000, 0.000000000000000000 ) ) ;
#17736=VECTOR ( 'NONE', #4477, 1000.000000000000000 ) ;
#17741=ADVANCED_FACE ( 'NONE', ( #6402 ), #17693, .F. ) ;
#17746=CARTESIAN_POINT ( 'NONE',  ( -0.4000000000000000222, 2.399999999999999911, 5.100000000000000533 ) ) ;
#17784=ORIENTED_EDGE ( 'NONE', *, *, #10277, .F. ) ;
#17804=ORIENTED_EDGE ( 'NONE', *, *, #701, .T. ) ;
#17827=DIRECTION ( 'NONE',  ( -2.220446049250309876E-16, 1.000000000000000000, 0.000000000000000000 ) ) ;
#17841=FACE_OUTER_BOUND ( 'NONE', #5318, .T. ) ;
#17843=LINE ( 'NONE', #2129, #13181 ) ;
#17849=CARTESIAN_POINT ( 'NONE',  ( 0.5500000000000000444, 6.450000000000000178, 1.600000000000000089 ) ) ;
#17857=ORIENTED_EDGE ( 'NONE', *, *, #10271, .F. ) ;
#17873=CARTESIAN_POINT ( 'NONE',  ( 0.5000000000000000000, 4.631370849898480024, 6.100000000000000533 ) ) ;
#17880=EDGE_LOOP ( 'NONE', ( #14641, #16133, #1327, #17324 ) ) ;
#17898=AXIS2_PLACEMENT_3D ( 'NONE', #5181, #16202, #16476 ) ;
#17907=ORIENTED_EDGE ( 'NONE', *, *, #7336, .T. ) ;
#17914=CARTESIAN_POINT ( 'NONE',  ( 1.000000000000000000, -8.000000000000000000, 5.700000000000000178 ) ) ;
#17927=LINE ( 'NONE', #16570, #16689 ) ;
#17931=DIRECTION ( 'NONE',  ( 0.000000000000000000, -1.000000000000000000, 0.000000000000000000 ) ) ;
#17934=VERTEX_POINT ( 'NONE', #2531 ) ;
#17936=VECTOR ( 'NONE', #440, 1000.000000000000000 ) ;
#17938=PLANE ( 'NONE',  #18223 ) ;
#17960=CARTESIAN_POINT ( 'NONE',  ( 1.000000000000000000, -5.500000000000000000, 5.100000000000000533 ) ) ;
#17976=ADVANCED_FACE ( 'NONE', ( #4372 ), #217, .F. ) ;
#17991=DIRECTION ( 'NONE',  ( -0.7071067811865480168, 0.7071067811865470176, 0.000000000000000000 ) ) ;
#17995=EDGE_LOOP ( 'NONE', ( #12898, #15874, #2959, #11779, #14745, #16308, #12729, #6651 ) ) ;
#18000=LINE ( 'NONE', #9592, #5643 ) ;
#18003=FACE_OUTER_BOUND ( 'NONE', #10857, .T. ) ;
#18019=VERTEX_POINT ( 'NONE', #8724 ) ;
#18020=DIRECTION ( 'NONE',  ( -1.644774851296529842E-16, 1.000000000000000000, 0.000000000000000000 ) ) ;
#18026=VECTOR ( 'NONE', #17529, 1000.000000000000000 ) ;
#18027=ADVANCED_FACE ( 'NONE', ( #1423 ), #5949, .T. ) ;
#18033=CARTESIAN_POINT ( 'NONE',  ( -1.800000000000000044, 0.5999999999999999778, 7.599999999999999645 ) ) ;
#18043=ORIENTED_EDGE ( 'NONE', *, *, #6779, .T. ) ;
#18049=CARTESIAN_POINT ( 'NONE',  ( -1.000000000000000000, -8.000000000000000000, 3.700000000000000178 ) ) ;
#18055=DIRECTION ( 'NONE',  ( 0.000000000000000000, 0.000000000000000000, -1.000000000000000000 ) ) ;
#18057=EDGE_CURVE ( 'NONE', #2805, #6472, #16122, .T. ) ;
#18067=LINE ( 'NONE', #16699, #6681 ) ;
#18088=EDGE_LOOP ( 'NONE', ( #11188, #9962, #15365, #5659 ) ) ;
#18092=PLANE ( 'NONE',  #17358 ) ;
#18095=CARTESIAN_POINT ( 'NONE',  ( -1.800000000000000044, 0.5999999999999999778, 7.599999999999999645 ) ) ;
#18097=ORIENTED_EDGE ( 'NONE', *, *, #12782, .F. ) ;
#18105=FACE_OUTER_BOUND ( 'NONE', #1397, .T. ) ;
#18113=CARTESIAN_POINT ( 'NONE',  ( 0.5000000000000000000, 3.500000000000000000, 6.100000000000000533 ) ) ;
#18114=EDGE_CURVE ( 'NONE', #16120, #8561, #15643, .T. ) ;
#18121=DIRECTION ( 'NONE',  ( 1.470526319674639030E-16, 0.7492686492653546360, -0.6622661785325225647 ) ) ;
#18126=COLOUR_RGB ( '', 0.66274510, 0.83137255, 0.94901961) ;
#18151=ORIENTED_EDGE ( 'NONE', *, *, #3688, .F. ) ;
#18178=CARTESIAN_POINT ( 'NONE',  ( -1.800000000000000044, 7.799999999999999822, 7.599999999999999645 ) ) ;
#18179=ORIENTED_EDGE ( 'NONE', *, *, #12544, .T. ) ;
#18193=ORIENTED_EDGE ( 'NONE', *, *, #6878, .F. ) ;
#18194=VECTOR ( 'NONE', #7726, 1000.000000000000000 ) ;
#18206=CARTESIAN_POINT ( 'NONE',  ( 0.4000000000000000222, -1.399999999999999911, 5.100000000000000533 ) ) ;
#18212=ADVANCED_FACE ( 'NONE', ( #4812 ), #14831, .F. ) ;
#18216=EDGE_CURVE ( 'NONE', #17934, #16120, #16311, .T. ) ;
#18218=CARTESIAN_POINT ( 'NONE',  ( -0.9000000000000000222, 2.050000000000000266, 3.600000000000000089 ) ) ;
#18223=AXIS2_PLACEMENT_3D ( 'NONE', #13788, #3970, #16664 ) ;
#18241=CARTESIAN_POINT ( 'NONE',  ( -1.399999999999999911, -5.000000000000000000, 6.100000000000000533 ) ) ;
#18242=ORIENTED_EDGE ( 'NONE', *, *, #17102, .T. ) ;
#18249=ORIENTED_EDGE ( 'NONE', *, *, #7236, .T. ) ;
#18257=CARTESIAN_POINT ( 'NONE',  ( -1.000000000000000000, -6.000000000000000000, 3.299999999999999822 ) ) ;
#18261=ORIENTED_EDGE ( 'NONE', *, *, #10281, .F. ) ;
#18274=FACE_OUTER_BOUND ( 'NONE', #7862, .T. ) ;
#18279=VECTOR ( 'NONE', #8855, 1000.000000000000000 ) ;
#18285=CARTESIAN_POINT ( 'NONE',  ( -1.800000000000000044, 0.5999999999999999778, 1.600000000000000089 ) ) ;
#18287=EDGE_CURVE ( 'NONE', #4545, #8308, #14052, .T. ) ;
#18290=CARTESIAN_POINT ( 'NONE',  ( -1.000000000000000000, -8.000000000000000000, 5.700000000000000178 ) ) ;
ENDSEC;
END-ISO-10303-21;
